ISO-10303-21;
HEADER;
/* Generated by software containing ST-Developer
 * from STEP Tools, Inc. (www.steptools.com) 
 */
/* OPTION: using custom renumber hook */

FILE_DESCRIPTION(
/* description */ ('STEP AP242 Edition 2', 'CAx-IF Rec.Pracs.---Representation and Presentation of Product Manufa
cturing Information (PMI)---4.0---2014-10-13', 'CAx-IF Rec.Pracs.---3D Tessellated Geometry---0.4---2014-09-14', '2;1', 'CAx-IF Rec.Pracs.---User Defined Attributes---1.5---2016-08-15'),
/* implementation_level */ '2;1');

FILE_NAME(
/* name */ 'Top_acces_nozzle_supporter.step',
/* time_stamp */ '2026-10-08T12:15:07Z',
/* author */ (''),
/* organization */ (''),
/* preprocessor_version */ 'ST-DEVELOPER v20',
/* originating_system */ 'ONSHAPE BY PTC INC, 1.221',
/* authorisation */ '  ');

FILE_SCHEMA (('AP242_MANAGED_MODEL_BASED_3D_ENGINEERING_MIM_LF { 1 0 10303 442 3 1 4 }'));
ENDSEC;

DATA;
#201=SHAPE_REPRESENTATION_RELATIONSHIP('','',#13775,#228);
#228=ADVANCED_BREP_SHAPE_REPRESENTATION('',(#13719),#45465);
#255=TOROIDAL_SURFACE('',#13902,0.00555,0.001);
#337=CIRCLE('',#13807,0.00455);
#338=CIRCLE('',#13808,0.00241485272203757);
#339=CIRCLE('',#13809,0.00241485272203757);
#340=CIRCLE('',#13810,0.00262);
#341=CIRCLE('',#13812,0.00262);
#342=CIRCLE('',#13813,0.00455);
#343=CIRCLE('',#13815,0.00455);
#344=CIRCLE('',#13816,0.00505);
#345=CIRCLE('',#13820,0.001);
#346=CIRCLE('',#13821,0.001);
#347=CIRCLE('',#13825,0.001);
#348=CIRCLE('',#13826,0.001);
#349=CIRCLE('',#13830,0.001);
#350=CIRCLE('',#13831,0.001);
#351=CIRCLE('',#13833,0.00297688);
#352=CIRCLE('',#13834,0.001397);
#353=CIRCLE('',#13836,0.00297688);
#354=CIRCLE('',#13837,0.001397);
#355=CIRCLE('',#13839,0.00297688);
#356=CIRCLE('',#13840,0.001397);
#357=CIRCLE('',#13842,0.00297688);
#358=CIRCLE('',#13843,0.001397);
#359=CIRCLE('',#13845,0.00400000000000387);
#360=CIRCLE('',#13846,0.00400000000000265);
#361=CIRCLE('',#13847,0.004);
#362=CIRCLE('',#13848,0.00755);
#363=CIRCLE('',#13849,0.05);
#364=CIRCLE('',#13850,0.001397);
#365=CIRCLE('',#13851,0.001397);
#366=CIRCLE('',#13852,0.001397);
#367=CIRCLE('',#13853,0.001397);
#368=CIRCLE('',#13854,0.001);
#369=CIRCLE('',#13855,0.001);
#370=CIRCLE('',#13856,0.001);
#371=CIRCLE('',#13857,0.01);
#372=CIRCLE('',#13859,0.00400000000000387);
#373=CIRCLE('',#13860,0.004);
#374=CIRCLE('',#13861,0.05);
#375=CIRCLE('',#13862,0.00755);
#376=CIRCLE('',#13863,0.00400000000000265);
#377=CIRCLE('',#13864,0.00297688);
#378=CIRCLE('',#13865,0.00297688);
#379=CIRCLE('',#13866,0.00297688);
#380=CIRCLE('',#13867,0.00297688);
#381=CIRCLE('',#13868,0.001);
#382=CIRCLE('',#13869,0.001);
#383=CIRCLE('',#13870,0.001);
#384=CIRCLE('',#13871,0.01);
#385=CIRCLE('',#13873,0.00755);
#386=CIRCLE('',#13874,0.00505);
#387=CIRCLE('',#13876,0.00755);
#388=CIRCLE('',#13877,0.00555);
#389=CIRCLE('',#13879,0.00455);
#390=CIRCLE('',#13901,0.00241485272203757);
#1062=B_SPLINE_CURVE_WITH_KNOTS('',3,(#19536,#19537,#19538,#19539),
 .UNSPECIFIED.,.F.,.F.,(4,4),(0.,0.00278168915164146),.UNSPECIFIED.);
#1063=B_SPLINE_CURVE_WITH_KNOTS('',2,(#19634,#19635,#19636),
 .UNSPECIFIED.,.F.,.F.,(3,3),(0.,1.),.UNSPECIFIED.);
#1064=B_SPLINE_CURVE_WITH_KNOTS('',2,(#19641,#19642,#19643),
 .UNSPECIFIED.,.F.,.F.,(3,3),(0.,1.),.UNSPECIFIED.);
#1201=PLANE('',#13804);
#1202=PLANE('',#13805);
#1203=PLANE('',#13806);
#1204=PLANE('',#13811);
#1205=PLANE('',#13814);
#1206=PLANE('',#13817);
#1207=PLANE('',#13818);
#1208=PLANE('',#13822);
#1209=PLANE('',#13823);
#1210=PLANE('',#13827);
#1211=PLANE('',#13828);
#1212=PLANE('',#13832);
#1213=PLANE('',#13835);
#1214=PLANE('',#13838);
#1215=PLANE('',#13841);
#1216=PLANE('',#13844);
#1217=PLANE('',#13858);
#1218=PLANE('',#13872);
#1219=PLANE('',#13875);
#1538=CYLINDRICAL_SURFACE('',#13803,0.00322675153453757);
#1539=CYLINDRICAL_SURFACE('',#13819,0.001);
#1540=CYLINDRICAL_SURFACE('',#13824,0.001);
#1541=CYLINDRICAL_SURFACE('',#13829,0.001);
#1542=CYLINDRICAL_SURFACE('',#13878,0.00455);
#1543=CYLINDRICAL_SURFACE('',#13880,0.00455);
#1544=CYLINDRICAL_SURFACE('',#13881,0.00755);
#1545=CYLINDRICAL_SURFACE('',#13882,0.00755);
#1546=CYLINDRICAL_SURFACE('',#13883,0.05);
#1547=CYLINDRICAL_SURFACE('',#13884,0.004);
#1548=CYLINDRICAL_SURFACE('',#13885,0.00400000000000265);
#1549=CYLINDRICAL_SURFACE('',#13886,0.00400000000000387);
#1550=CYLINDRICAL_SURFACE('',#13887,0.001397);
#1551=CYLINDRICAL_SURFACE('',#13888,0.00297688);
#1552=CYLINDRICAL_SURFACE('',#13889,0.001397);
#1553=CYLINDRICAL_SURFACE('',#13890,0.00297688);
#1554=CYLINDRICAL_SURFACE('',#13891,0.001397);
#1555=CYLINDRICAL_SURFACE('',#13892,0.00297688);
#1556=CYLINDRICAL_SURFACE('',#13893,0.001397);
#1557=CYLINDRICAL_SURFACE('',#13894,0.00297688);
#1558=CYLINDRICAL_SURFACE('',#13895,0.001);
#1559=CYLINDRICAL_SURFACE('',#13896,0.001);
#1560=CYLINDRICAL_SURFACE('',#13897,0.001);
#1561=CYLINDRICAL_SURFACE('',#13898,0.01);
#1562=CYLINDRICAL_SURFACE('',#13899,0.00505);
#1563=CYLINDRICAL_SURFACE('',#13900,0.00241485272203757);
#1826=(
BOUNDED_CURVE()
B_SPLINE_CURVE(2,(#19227,#19228,#19229,#19230,#19231,#19232,#19233,#19234,
#19235),.UNSPECIFIED.,.F.,.F.)
B_SPLINE_CURVE_WITH_KNOTS((3,2,2,2,3),(0.,0.03125,0.0625,0.09375,0.125),
 .UNSPECIFIED.)
CURVE()
GEOMETRIC_REPRESENTATION_ITEM()
RATIONAL_B_SPLINE_CURVE((1.,0.923879532511287,1.,0.923879532511287,1.,0.923879532511287,
1.,0.923879532511287,1.))
REPRESENTATION_ITEM('')
);
#1827=(
BOUNDED_CURVE()
B_SPLINE_CURVE(2,(#19237,#19238,#19239,#19240,#19241,#19242,#19243,#19244,
#19245),.UNSPECIFIED.,.F.,.F.)
B_SPLINE_CURVE_WITH_KNOTS((3,2,2,2,3),(0.125,0.15625,0.1875,0.21875,0.25),
 .UNSPECIFIED.)
CURVE()
GEOMETRIC_REPRESENTATION_ITEM()
RATIONAL_B_SPLINE_CURVE((1.,0.923879532511287,1.,0.923879532511287,1.,0.923879532511287,
1.,0.923879532511287,1.))
REPRESENTATION_ITEM('')
);
#1828=(
BOUNDED_CURVE()
B_SPLINE_CURVE(2,(#19247,#19248,#19249,#19250,#19251,#19252,#19253,#19254,
#19255),.UNSPECIFIED.,.F.,.F.)
B_SPLINE_CURVE_WITH_KNOTS((3,2,2,2,3),(0.25,0.28125,0.3125,0.34375,0.375),
 .UNSPECIFIED.)
CURVE()
GEOMETRIC_REPRESENTATION_ITEM()
RATIONAL_B_SPLINE_CURVE((1.,0.923879532511287,1.,0.923879532511287,1.,0.923879532511287,
1.,0.923879532511287,1.))
REPRESENTATION_ITEM('')
);
#1829=(
BOUNDED_CURVE()
B_SPLINE_CURVE(2,(#19257,#19258,#19259,#19260,#19261,#19262,#19263,#19264,
#19265),.UNSPECIFIED.,.F.,.F.)
B_SPLINE_CURVE_WITH_KNOTS((3,2,2,2,3),(0.375,0.40625,0.4375,0.46875,0.5),
 .UNSPECIFIED.)
CURVE()
GEOMETRIC_REPRESENTATION_ITEM()
RATIONAL_B_SPLINE_CURVE((1.,0.923879532511287,1.,0.923879532511287,1.,0.923879532511287,
1.,0.923879532511287,1.))
REPRESENTATION_ITEM('')
);
#1830=(
BOUNDED_CURVE()
B_SPLINE_CURVE(2,(#19267,#19268,#19269,#19270,#19271,#19272,#19273,#19274,
#19275),.UNSPECIFIED.,.F.,.F.)
B_SPLINE_CURVE_WITH_KNOTS((3,2,2,2,3),(0.5,0.53125,0.5625,0.59375,0.625),
 .UNSPECIFIED.)
CURVE()
GEOMETRIC_REPRESENTATION_ITEM()
RATIONAL_B_SPLINE_CURVE((1.,0.923879532511287,1.,0.923879532511287,1.,0.923879532511287,
1.,0.923879532511287,1.))
REPRESENTATION_ITEM('')
);
#1831=(
BOUNDED_CURVE()
B_SPLINE_CURVE(2,(#19277,#19278,#19279,#19280,#19281,#19282,#19283,#19284,
#19285),.UNSPECIFIED.,.F.,.F.)
B_SPLINE_CURVE_WITH_KNOTS((3,2,2,2,3),(0.625,0.65625,0.6875,0.71875,0.75),
 .UNSPECIFIED.)
CURVE()
GEOMETRIC_REPRESENTATION_ITEM()
RATIONAL_B_SPLINE_CURVE((1.,0.923879532511287,1.,0.923879532511287,1.,0.923879532511287,
1.,0.923879532511287,1.))
REPRESENTATION_ITEM('')
);
#1832=(
BOUNDED_CURVE()
B_SPLINE_CURVE(2,(#19287,#19288,#19289,#19290,#19291,#19292,#19293,#19294,
#19295),.UNSPECIFIED.,.F.,.F.)
B_SPLINE_CURVE_WITH_KNOTS((3,2,2,2,3),(0.75,0.78125,0.8125,0.84375,0.875),
 .UNSPECIFIED.)
CURVE()
GEOMETRIC_REPRESENTATION_ITEM()
RATIONAL_B_SPLINE_CURVE((1.,0.923879532511287,1.,0.923879532511287,1.,0.923879532511287,
1.,0.923879532511287,1.))
REPRESENTATION_ITEM('')
);
#1833=(
BOUNDED_CURVE()
B_SPLINE_CURVE(2,(#19299,#19300,#19301,#19302,#19303,#19304,#19305,#19306,
#19307,#19308,#19309,#19310,#19311,#19312,#19313,#19314,#19315,#19316,#19317,
#19318,#19319,#19320,#19321,#19322,#19323,#19324,#19325,#19326,#19327,#19328,
#19329,#19330,#19331,#19332,#19333,#19334,#19335,#19336,#19337,#19338,#19339,
#19340,#19341,#19342,#19343,#19344,#19345,#19346,#19347,#19348,#19349,#19350,
#19351,#19352,#19353,#19354,#19355),.UNSPECIFIED.,.F.,.F.)
B_SPLINE_CURVE_WITH_KNOTS((3,2,2,2,2,2,2,2,2,2,2,2,2,2,2,2,2,2,2,2,2,2,
2,2,2,2,2,2,3),(0.,0.03125,0.0625,0.09375,0.125,0.15625,0.1875,0.21875,
0.25,0.28125,0.3125,0.34375,0.375,0.40625,0.4375,0.46875,0.5,0.53125,0.5625,
0.59375,0.625,0.65625,0.6875,0.71875,0.75,0.78125,0.8125,0.84375,0.875),
 .UNSPECIFIED.)
CURVE()
GEOMETRIC_REPRESENTATION_ITEM()
RATIONAL_B_SPLINE_CURVE((1.,0.923879532511287,1.,0.923879532511287,1.,0.923879532511287,
1.,0.923879532511287,1.,0.923879532511287,1.,0.923879532511287,1.,0.923879532511287,
1.,0.923879532511287,1.,0.923879532511287,1.,0.923879532511287,1.,0.923879532511287,
1.,0.923879532511287,1.,0.923879532511287,1.,0.923879532511287,1.,0.923879532511287,
1.,0.923879532511287,1.,0.923879532511287,1.,0.923879532511287,1.,0.923879532511287,
1.,0.923879532511287,1.,0.923879532511287,1.,0.923879532511287,1.,0.923879532511287,
1.,0.923879532511287,1.,0.923879532511287,1.,0.923879532511287,1.,0.923879532511287,
1.,0.923879532511287,1.))
REPRESENTATION_ITEM('')
);
#1834=(
BOUNDED_CURVE()
B_SPLINE_CURVE(2,(#19361,#19362,#19363,#19364,#19365,#19366,#19367,#19368,
#19369,#19370,#19371,#19372,#19373,#19374,#19375,#19376,#19377,#19378,#19379,
#19380,#19381,#19382,#19383,#19384,#19385,#19386,#19387,#19388,#19389,#19390,
#19391,#19392,#19393,#19394,#19395,#19396,#19397,#19398,#19399,#19400,#19401,
#19402,#19403,#19404,#19405,#19406,#19407,#19408,#19409,#19410,#19411,#19412,
#19413,#19414,#19415,#19416,#19417),.UNSPECIFIED.,.F.,.F.)
B_SPLINE_CURVE_WITH_KNOTS((3,2,2,2,2,2,2,2,2,2,2,2,2,2,2,2,2,2,2,2,2,2,
2,2,2,2,2,2,3),(0.,0.03125,0.0625,0.09375,0.125,0.15625,0.1875,0.21875,
0.25,0.28125,0.3125,0.34375,0.375,0.40625,0.4375,0.46875,0.5,0.53125,0.5625,
0.59375,0.625,0.65625,0.6875,0.71875,0.75,0.78125,0.8125,0.84375,0.875),
 .UNSPECIFIED.)
CURVE()
GEOMETRIC_REPRESENTATION_ITEM()
RATIONAL_B_SPLINE_CURVE((1.,0.923879532511287,1.,0.923879532511287,1.,0.923879532511287,
1.,0.923879532511287,1.,0.923879532511287,1.,0.923879532511287,1.,0.923879532511287,
1.,0.923879532511287,1.,0.923879532511287,1.,0.923879532511287,1.,0.923879532511287,
1.,0.923879532511287,1.,0.923879532511287,1.,0.923879532511287,1.,0.923879532511287,
1.,0.923879532511287,1.,0.923879532511287,1.,0.923879532511287,1.,0.923879532511287,
1.,0.923879532511287,1.,0.923879532511287,1.,0.923879532511287,1.,0.923879532511287,
1.,0.923879532511287,1.,0.923879532511287,1.,0.923879532511287,1.,0.923879532511287,
1.,0.923879532511287,1.))
REPRESENTATION_ITEM('')
);
#1835=(
BOUNDED_CURVE()
B_SPLINE_CURVE(2,(#19543,#19544,#19545,#19546,#19547,#19548,#19549,#19550,
#19551),.UNSPECIFIED.,.F.,.F.)
B_SPLINE_CURVE_WITH_KNOTS((3,2,2,2,3),(0.75,0.78125,0.8125,0.84375,0.875),
 .UNSPECIFIED.)
CURVE()
GEOMETRIC_REPRESENTATION_ITEM()
RATIONAL_B_SPLINE_CURVE((1.,0.923879532511287,1.,0.923879532511287,1.,0.923879532511287,
1.,0.923879532511287,1.))
REPRESENTATION_ITEM('')
);
#1836=(
BOUNDED_CURVE()
B_SPLINE_CURVE(2,(#19553,#19554,#19555,#19556,#19557,#19558,#19559,#19560,
#19561),.UNSPECIFIED.,.F.,.F.)
B_SPLINE_CURVE_WITH_KNOTS((3,2,2,2,3),(0.625,0.65625,0.6875,0.71875,0.75),
 .UNSPECIFIED.)
CURVE()
GEOMETRIC_REPRESENTATION_ITEM()
RATIONAL_B_SPLINE_CURVE((1.,0.923879532511287,1.,0.923879532511287,1.,0.923879532511287,
1.,0.923879532511287,1.))
REPRESENTATION_ITEM('')
);
#1837=(
BOUNDED_CURVE()
B_SPLINE_CURVE(2,(#19563,#19564,#19565,#19566,#19567,#19568,#19569,#19570,
#19571),.UNSPECIFIED.,.F.,.F.)
B_SPLINE_CURVE_WITH_KNOTS((3,2,2,2,3),(0.5,0.53125,0.5625,0.59375,0.625),
 .UNSPECIFIED.)
CURVE()
GEOMETRIC_REPRESENTATION_ITEM()
RATIONAL_B_SPLINE_CURVE((1.,0.923879532511287,1.,0.923879532511287,1.,0.923879532511287,
1.,0.923879532511287,1.))
REPRESENTATION_ITEM('')
);
#1838=(
BOUNDED_CURVE()
B_SPLINE_CURVE(2,(#19573,#19574,#19575,#19576,#19577,#19578,#19579,#19580,
#19581),.UNSPECIFIED.,.F.,.F.)
B_SPLINE_CURVE_WITH_KNOTS((3,2,2,2,3),(0.375,0.40625,0.4375,0.46875,0.5),
 .UNSPECIFIED.)
CURVE()
GEOMETRIC_REPRESENTATION_ITEM()
RATIONAL_B_SPLINE_CURVE((1.,0.923879532511287,1.,0.923879532511287,1.,0.923879532511287,
1.,0.923879532511287,1.))
REPRESENTATION_ITEM('')
);
#1839=(
BOUNDED_CURVE()
B_SPLINE_CURVE(2,(#19583,#19584,#19585,#19586,#19587,#19588,#19589,#19590,
#19591),.UNSPECIFIED.,.F.,.F.)
B_SPLINE_CURVE_WITH_KNOTS((3,2,2,2,3),(0.25,0.28125,0.3125,0.34375,0.375),
 .UNSPECIFIED.)
CURVE()
GEOMETRIC_REPRESENTATION_ITEM()
RATIONAL_B_SPLINE_CURVE((1.,0.923879532511287,1.,0.923879532511287,1.,0.923879532511287,
1.,0.923879532511287,1.))
REPRESENTATION_ITEM('')
);
#1840=(
BOUNDED_CURVE()
B_SPLINE_CURVE(2,(#19593,#19594,#19595,#19596,#19597,#19598,#19599,#19600,
#19601),.UNSPECIFIED.,.F.,.F.)
B_SPLINE_CURVE_WITH_KNOTS((3,2,2,2,3),(0.125,0.15625,0.1875,0.21875,0.25),
 .UNSPECIFIED.)
CURVE()
GEOMETRIC_REPRESENTATION_ITEM()
RATIONAL_B_SPLINE_CURVE((1.,0.923879532511287,1.,0.923879532511287,1.,0.923879532511287,
1.,0.923879532511287,1.))
REPRESENTATION_ITEM('')
);
#1841=(
BOUNDED_CURVE()
B_SPLINE_CURVE(2,(#19603,#19604,#19605,#19606,#19607,#19608,#19609),
 .UNSPECIFIED.,.F.,.F.)
B_SPLINE_CURVE_WITH_KNOTS((3,2,2,3),(0.0418443486222184,0.0625,0.09375,
0.125),.UNSPECIFIED.)
CURVE()
GEOMETRIC_REPRESENTATION_ITEM()
RATIONAL_B_SPLINE_CURVE((0.965885064534014,0.94968582914686,1.,0.923879532511287,
1.,0.923879532511287,1.))
REPRESENTATION_ITEM('')
);
#1966=ORIENTED_EDGE('',*,*,#5630,.T.);
#1967=ORIENTED_EDGE('',*,*,#5631,.T.);
#1968=ORIENTED_EDGE('',*,*,#5632,.T.);
#1969=ORIENTED_EDGE('',*,*,#5633,.T.);
#1970=ORIENTED_EDGE('',*,*,#5634,.T.);
#1971=ORIENTED_EDGE('',*,*,#5635,.T.);
#1972=ORIENTED_EDGE('',*,*,#5636,.T.);
#1973=ORIENTED_EDGE('',*,*,#5637,.T.);
#1974=ORIENTED_EDGE('',*,*,#5638,.T.);
#1975=ORIENTED_EDGE('',*,*,#5639,.F.);
#1976=ORIENTED_EDGE('',*,*,#5640,.T.);
#1977=ORIENTED_EDGE('',*,*,#5639,.T.);
#1978=ORIENTED_EDGE('',*,*,#5641,.T.);
#1979=ORIENTED_EDGE('',*,*,#5642,.F.);
#1980=ORIENTED_EDGE('',*,*,#5641,.F.);
#1981=ORIENTED_EDGE('',*,*,#5638,.F.);
#1982=ORIENTED_EDGE('',*,*,#5643,.F.);
#1983=ORIENTED_EDGE('',*,*,#5644,.F.);
#1984=ORIENTED_EDGE('',*,*,#5645,.T.);
#1985=ORIENTED_EDGE('',*,*,#5646,.T.);
#1986=ORIENTED_EDGE('',*,*,#5642,.T.);
#1987=ORIENTED_EDGE('',*,*,#5644,.T.);
#1988=ORIENTED_EDGE('',*,*,#5647,.F.);
#1989=ORIENTED_EDGE('',*,*,#5648,.F.);
#1990=ORIENTED_EDGE('',*,*,#5649,.F.);
#1991=ORIENTED_EDGE('',*,*,#5650,.F.);
#1992=ORIENTED_EDGE('',*,*,#5651,.F.);
#1993=ORIENTED_EDGE('',*,*,#5652,.F.);
#1994=ORIENTED_EDGE('',*,*,#5653,.F.);
#1995=ORIENTED_EDGE('',*,*,#5654,.F.);
#1996=ORIENTED_EDGE('',*,*,#5630,.F.);
#1997=ORIENTED_EDGE('',*,*,#5640,.F.);
#1998=ORIENTED_EDGE('',*,*,#5646,.F.);
#1999=ORIENTED_EDGE('',*,*,#5655,.F.);
#2000=ORIENTED_EDGE('',*,*,#5656,.T.);
#2001=ORIENTED_EDGE('',*,*,#5657,.F.);
#2002=ORIENTED_EDGE('',*,*,#5655,.T.);
#2003=ORIENTED_EDGE('',*,*,#5645,.F.);
#2004=ORIENTED_EDGE('',*,*,#5658,.F.);
#2005=ORIENTED_EDGE('',*,*,#5659,.T.);
#2006=ORIENTED_EDGE('',*,*,#5660,.T.);
#2007=ORIENTED_EDGE('',*,*,#5661,.F.);
#2008=ORIENTED_EDGE('',*,*,#5662,.T.);
#2009=ORIENTED_EDGE('',*,*,#5661,.T.);
#2010=ORIENTED_EDGE('',*,*,#5663,.T.);
#2011=ORIENTED_EDGE('',*,*,#5664,.T.);
#2012=ORIENTED_EDGE('',*,*,#5665,.T.);
#2013=ORIENTED_EDGE('',*,*,#5666,.T.);
#2014=ORIENTED_EDGE('',*,*,#5667,.F.);
#2015=ORIENTED_EDGE('',*,*,#5668,.F.);
#2016=ORIENTED_EDGE('',*,*,#5669,.T.);
#2017=ORIENTED_EDGE('',*,*,#5670,.T.);
#2018=ORIENTED_EDGE('',*,*,#5671,.F.);
#2019=ORIENTED_EDGE('',*,*,#5672,.F.);
#2020=ORIENTED_EDGE('',*,*,#5673,.T.);
#2021=ORIENTED_EDGE('',*,*,#5674,.T.);
#2022=ORIENTED_EDGE('',*,*,#5669,.F.);
#2023=ORIENTED_EDGE('',*,*,#5675,.F.);
#2024=ORIENTED_EDGE('',*,*,#5671,.T.);
#2025=ORIENTED_EDGE('',*,*,#5676,.T.);
#2026=ORIENTED_EDGE('',*,*,#5677,.F.);
#2027=ORIENTED_EDGE('',*,*,#5678,.F.);
#2028=ORIENTED_EDGE('',*,*,#5679,.T.);
#2029=ORIENTED_EDGE('',*,*,#5680,.T.);
#2030=ORIENTED_EDGE('',*,*,#5681,.F.);
#2031=ORIENTED_EDGE('',*,*,#5682,.F.);
#2032=ORIENTED_EDGE('',*,*,#5683,.T.);
#2033=ORIENTED_EDGE('',*,*,#5684,.T.);
#2034=ORIENTED_EDGE('',*,*,#5679,.F.);
#2035=ORIENTED_EDGE('',*,*,#5685,.F.);
#2036=ORIENTED_EDGE('',*,*,#5681,.T.);
#2037=ORIENTED_EDGE('',*,*,#5686,.T.);
#2038=ORIENTED_EDGE('',*,*,#5687,.F.);
#2039=ORIENTED_EDGE('',*,*,#5688,.F.);
#2040=ORIENTED_EDGE('',*,*,#5689,.T.);
#2041=ORIENTED_EDGE('',*,*,#5690,.T.);
#2042=ORIENTED_EDGE('',*,*,#5691,.F.);
#2043=ORIENTED_EDGE('',*,*,#5692,.F.);
#2044=ORIENTED_EDGE('',*,*,#5693,.T.);
#2045=ORIENTED_EDGE('',*,*,#5694,.T.);
#2046=ORIENTED_EDGE('',*,*,#5689,.F.);
#2047=ORIENTED_EDGE('',*,*,#5695,.F.);
#2048=ORIENTED_EDGE('',*,*,#5691,.T.);
#2049=ORIENTED_EDGE('',*,*,#5696,.T.);
#2050=ORIENTED_EDGE('',*,*,#5697,.F.);
#2051=ORIENTED_EDGE('',*,*,#5698,.T.);
#2052=ORIENTED_EDGE('',*,*,#5699,.F.);
#2053=ORIENTED_EDGE('',*,*,#5700,.T.);
#2054=ORIENTED_EDGE('',*,*,#5701,.F.);
#2055=ORIENTED_EDGE('',*,*,#5702,.T.);
#2056=ORIENTED_EDGE('',*,*,#5703,.F.);
#2057=ORIENTED_EDGE('',*,*,#5704,.T.);
#2058=ORIENTED_EDGE('',*,*,#5705,.T.);
#2059=ORIENTED_EDGE('',*,*,#5706,.T.);
#2060=ORIENTED_EDGE('',*,*,#5707,.T.);
#2061=ORIENTED_EDGE('',*,*,#5708,.F.);
#2062=ORIENTED_EDGE('',*,*,#5709,.T.);
#2063=ORIENTED_EDGE('',*,*,#5710,.T.);
#2064=ORIENTED_EDGE('',*,*,#5711,.T.);
#2065=ORIENTED_EDGE('',*,*,#5712,.T.);
#2066=ORIENTED_EDGE('',*,*,#5692,.T.);
#2067=ORIENTED_EDGE('',*,*,#5695,.T.);
#2068=ORIENTED_EDGE('',*,*,#5688,.T.);
#2069=ORIENTED_EDGE('',*,*,#5713,.T.);
#2070=ORIENTED_EDGE('',*,*,#5682,.T.);
#2071=ORIENTED_EDGE('',*,*,#5685,.T.);
#2072=ORIENTED_EDGE('',*,*,#5678,.T.);
#2073=ORIENTED_EDGE('',*,*,#5714,.T.);
#2074=ORIENTED_EDGE('',*,*,#5672,.T.);
#2075=ORIENTED_EDGE('',*,*,#5675,.T.);
#2076=ORIENTED_EDGE('',*,*,#5668,.T.);
#2077=ORIENTED_EDGE('',*,*,#5715,.T.);
#2078=ORIENTED_EDGE('',*,*,#5716,.F.);
#2079=ORIENTED_EDGE('',*,*,#5717,.F.);
#2080=ORIENTED_EDGE('',*,*,#5718,.F.);
#2081=ORIENTED_EDGE('',*,*,#5719,.T.);
#2082=ORIENTED_EDGE('',*,*,#5720,.T.);
#2083=ORIENTED_EDGE('',*,*,#5721,.F.);
#2084=ORIENTED_EDGE('',*,*,#5722,.F.);
#2085=ORIENTED_EDGE('',*,*,#5723,.F.);
#2086=ORIENTED_EDGE('',*,*,#5724,.F.);
#2087=ORIENTED_EDGE('',*,*,#5725,.F.);
#2088=ORIENTED_EDGE('',*,*,#5694,.F.);
#2089=ORIENTED_EDGE('',*,*,#5690,.F.);
#2090=ORIENTED_EDGE('',*,*,#5726,.F.);
#2091=ORIENTED_EDGE('',*,*,#5686,.F.);
#2092=ORIENTED_EDGE('',*,*,#5684,.F.);
#2093=ORIENTED_EDGE('',*,*,#5680,.F.);
#2094=ORIENTED_EDGE('',*,*,#5727,.F.);
#2095=ORIENTED_EDGE('',*,*,#5676,.F.);
#2096=ORIENTED_EDGE('',*,*,#5674,.F.);
#2097=ORIENTED_EDGE('',*,*,#5670,.F.);
#2098=ORIENTED_EDGE('',*,*,#5728,.F.);
#2099=ORIENTED_EDGE('',*,*,#5666,.F.);
#2100=ORIENTED_EDGE('',*,*,#5729,.T.);
#2101=ORIENTED_EDGE('',*,*,#5730,.T.);
#2102=ORIENTED_EDGE('',*,*,#5731,.F.);
#2103=ORIENTED_EDGE('',*,*,#5732,.F.);
#2104=ORIENTED_EDGE('',*,*,#5733,.T.);
#2105=ORIENTED_EDGE('',*,*,#5663,.F.);
#2106=ORIENTED_EDGE('',*,*,#5734,.T.);
#2107=ORIENTED_EDGE('',*,*,#5664,.F.);
#2108=ORIENTED_EDGE('',*,*,#5656,.F.);
#2109=ORIENTED_EDGE('',*,*,#5707,.F.);
#2110=ORIENTED_EDGE('',*,*,#5732,.T.);
#2111=ORIENTED_EDGE('',*,*,#5730,.F.);
#2112=ORIENTED_EDGE('',*,*,#5720,.F.);
#2113=ORIENTED_EDGE('',*,*,#5708,.T.);
#2114=ORIENTED_EDGE('',*,*,#5719,.F.);
#2115=ORIENTED_EDGE('',*,*,#5706,.F.);
#2116=ORIENTED_EDGE('',*,*,#5718,.T.);
#2117=ORIENTED_EDGE('',*,*,#5705,.F.);
#2118=ORIENTED_EDGE('',*,*,#5721,.T.);
#2119=ORIENTED_EDGE('',*,*,#5704,.F.);
#2120=ORIENTED_EDGE('',*,*,#5717,.T.);
#2121=ORIENTED_EDGE('',*,*,#5703,.T.);
#2122=ORIENTED_EDGE('',*,*,#5709,.F.);
#2123=ORIENTED_EDGE('',*,*,#5722,.T.);
#2124=ORIENTED_EDGE('',*,*,#5702,.F.);
#2125=ORIENTED_EDGE('',*,*,#5701,.T.);
#2126=ORIENTED_EDGE('',*,*,#5710,.F.);
#2127=ORIENTED_EDGE('',*,*,#5723,.T.);
#2128=ORIENTED_EDGE('',*,*,#5700,.F.);
#2129=ORIENTED_EDGE('',*,*,#5699,.T.);
#2130=ORIENTED_EDGE('',*,*,#5711,.F.);
#2131=ORIENTED_EDGE('',*,*,#5724,.T.);
#2132=ORIENTED_EDGE('',*,*,#5698,.F.);
#2133=ORIENTED_EDGE('',*,*,#5697,.T.);
#2134=ORIENTED_EDGE('',*,*,#5712,.F.);
#2135=ORIENTED_EDGE('',*,*,#5725,.T.);
#2136=ORIENTED_EDGE('',*,*,#5696,.F.);
#2137=ORIENTED_EDGE('',*,*,#5713,.F.);
#2138=ORIENTED_EDGE('',*,*,#5687,.T.);
#2139=ORIENTED_EDGE('',*,*,#5726,.T.);
#2140=ORIENTED_EDGE('',*,*,#5693,.F.);
#2141=ORIENTED_EDGE('',*,*,#5714,.F.);
#2142=ORIENTED_EDGE('',*,*,#5677,.T.);
#2143=ORIENTED_EDGE('',*,*,#5727,.T.);
#2144=ORIENTED_EDGE('',*,*,#5683,.F.);
#2145=ORIENTED_EDGE('',*,*,#5715,.F.);
#2146=ORIENTED_EDGE('',*,*,#5667,.T.);
#2147=ORIENTED_EDGE('',*,*,#5728,.T.);
#2148=ORIENTED_EDGE('',*,*,#5673,.F.);
#2149=ORIENTED_EDGE('',*,*,#5716,.T.);
#2150=ORIENTED_EDGE('',*,*,#5729,.F.);
#2151=ORIENTED_EDGE('',*,*,#5731,.T.);
#2152=ORIENTED_EDGE('',*,*,#5665,.F.);
#2153=ORIENTED_EDGE('',*,*,#5643,.T.);
#2154=ORIENTED_EDGE('',*,*,#5637,.F.);
#2155=ORIENTED_EDGE('',*,*,#5636,.F.);
#2156=ORIENTED_EDGE('',*,*,#5635,.F.);
#2157=ORIENTED_EDGE('',*,*,#5634,.F.);
#2158=ORIENTED_EDGE('',*,*,#5633,.F.);
#2159=ORIENTED_EDGE('',*,*,#5632,.F.);
#2160=ORIENTED_EDGE('',*,*,#5631,.F.);
#2161=ORIENTED_EDGE('',*,*,#5654,.T.);
#2162=ORIENTED_EDGE('',*,*,#5657,.T.);
#2163=ORIENTED_EDGE('',*,*,#5653,.T.);
#2164=ORIENTED_EDGE('',*,*,#5652,.T.);
#2165=ORIENTED_EDGE('',*,*,#5651,.T.);
#2166=ORIENTED_EDGE('',*,*,#5650,.T.);
#2167=ORIENTED_EDGE('',*,*,#5649,.T.);
#2168=ORIENTED_EDGE('',*,*,#5648,.T.);
#2169=ORIENTED_EDGE('',*,*,#5647,.T.);
#2170=ORIENTED_EDGE('',*,*,#5735,.F.);
#2171=ORIENTED_EDGE('',*,*,#5659,.F.);
#2172=ORIENTED_EDGE('',*,*,#5733,.F.);
#2173=ORIENTED_EDGE('',*,*,#5734,.F.);
#2174=ORIENTED_EDGE('',*,*,#5735,.T.);
#2175=ORIENTED_EDGE('',*,*,#5658,.T.);
#2176=ORIENTED_EDGE('',*,*,#5662,.F.);
#2177=ORIENTED_EDGE('',*,*,#5660,.F.);
#5630=EDGE_CURVE('',#7462,#7463,#8773,.T.);
#5631=EDGE_CURVE('',#7463,#7464,#1826,.T.);
#5632=EDGE_CURVE('',#7464,#7465,#1827,.T.);
#5633=EDGE_CURVE('',#7465,#7466,#1828,.T.);
#5634=EDGE_CURVE('',#7466,#7467,#1829,.T.);
#5635=EDGE_CURVE('',#7467,#7468,#1830,.T.);
#5636=EDGE_CURVE('',#7468,#7469,#1831,.T.);
#5637=EDGE_CURVE('',#7469,#7470,#1832,.T.);
#5638=EDGE_CURVE('',#7470,#7471,#8774,.T.);
#5639=EDGE_CURVE('',#7462,#7471,#1833,.T.);
#5640=EDGE_CURVE('',#7472,#7462,#8775,.T.);
#5641=EDGE_CURVE('',#7471,#7473,#8776,.T.);
#5642=EDGE_CURVE('',#7472,#7473,#1834,.T.);
#5643=EDGE_CURVE('',#7474,#7470,#8777,.T.);
#5644=EDGE_CURVE('',#7473,#7474,#8778,.T.);
#5645=EDGE_CURVE('',#7475,#7476,#1062,.T.);
#5646=EDGE_CURVE('',#7476,#7472,#8779,.T.);
#5647=EDGE_CURVE('',#7477,#7474,#1835,.T.);
#5648=EDGE_CURVE('',#7478,#7477,#1836,.T.);
#5649=EDGE_CURVE('',#7479,#7478,#1837,.T.);
#5650=EDGE_CURVE('',#7480,#7479,#1838,.T.);
#5651=EDGE_CURVE('',#7481,#7480,#1839,.T.);
#5652=EDGE_CURVE('',#7482,#7481,#1840,.T.);
#5653=EDGE_CURVE('',#7475,#7482,#1841,.T.);
#5654=EDGE_CURVE('',#7463,#7483,#8780,.T.);
#5655=EDGE_CURVE('',#7483,#7476,#8781,.T.);
#5656=EDGE_CURVE('',#7484,#7484,#337,.T.);
#5657=EDGE_CURVE('',#7483,#7475,#338,.T.);
#5658=EDGE_CURVE('',#7485,#7486,#1063,.T.);
#5659=EDGE_CURVE('',#7485,#7487,#339,.T.);
#5660=EDGE_CURVE('',#7487,#7488,#1064,.T.);
#5661=EDGE_CURVE('',#7486,#7488,#340,.T.);
#5662=EDGE_CURVE('',#7488,#7486,#341,.T.);
#5663=EDGE_CURVE('',#7489,#7489,#342,.T.);
#5664=EDGE_CURVE('',#7490,#7490,#343,.T.);
#5665=EDGE_CURVE('',#7491,#7491,#344,.T.);
#5666=EDGE_CURVE('',#7492,#7493,#8782,.T.);
#5667=EDGE_CURVE('',#7494,#7493,#8783,.T.);
#5668=EDGE_CURVE('',#7495,#7494,#8784,.T.);
#5669=EDGE_CURVE('',#7495,#7492,#8785,.T.);
#5670=EDGE_CURVE('',#7496,#7497,#8786,.T.);
#5671=EDGE_CURVE('',#7498,#7497,#8787,.T.);
#5672=EDGE_CURVE('',#7499,#7498,#8788,.T.);
#5673=EDGE_CURVE('',#7499,#7496,#8789,.T.);
#5674=EDGE_CURVE('',#7497,#7492,#345,.T.);
#5675=EDGE_CURVE('',#7498,#7495,#346,.T.);
#5676=EDGE_CURVE('',#7500,#7501,#8790,.T.);
#5677=EDGE_CURVE('',#7502,#7501,#8791,.T.);
#5678=EDGE_CURVE('',#7503,#7502,#8792,.T.);
#5679=EDGE_CURVE('',#7503,#7500,#8793,.T.);
#5680=EDGE_CURVE('',#7504,#7505,#8794,.T.);
#5681=EDGE_CURVE('',#7506,#7505,#8795,.T.);
#5682=EDGE_CURVE('',#7507,#7506,#8796,.T.);
#5683=EDGE_CURVE('',#7507,#7504,#8797,.T.);
#5684=EDGE_CURVE('',#7505,#7500,#347,.T.);
#5685=EDGE_CURVE('',#7506,#7503,#348,.T.);
#5686=EDGE_CURVE('',#7508,#7509,#8798,.T.);
#5687=EDGE_CURVE('',#7510,#7509,#8799,.T.);
#5688=EDGE_CURVE('',#7511,#7510,#8800,.T.);
#5689=EDGE_CURVE('',#7511,#7508,#8801,.T.);
#5690=EDGE_CURVE('',#7512,#7513,#8802,.T.);
#5691=EDGE_CURVE('',#7514,#7513,#8803,.T.);
#5692=EDGE_CURVE('',#7515,#7514,#8804,.T.);
#5693=EDGE_CURVE('',#7515,#7512,#8805,.T.);
#5694=EDGE_CURVE('',#7513,#7508,#349,.T.);
#5695=EDGE_CURVE('',#7514,#7511,#350,.T.);
#5696=EDGE_CURVE('',#7516,#7516,#351,.T.);
#5697=EDGE_CURVE('',#7517,#7517,#352,.T.);
#5698=EDGE_CURVE('',#7518,#7518,#353,.T.);
#5699=EDGE_CURVE('',#7519,#7519,#354,.T.);
#5700=EDGE_CURVE('',#7520,#7520,#355,.T.);
#5701=EDGE_CURVE('',#7521,#7521,#356,.T.);
#5702=EDGE_CURVE('',#7522,#7522,#357,.T.);
#5703=EDGE_CURVE('',#7523,#7523,#358,.T.);
#5704=EDGE_CURVE('',#7524,#7524,#359,.T.);
#5705=EDGE_CURVE('',#7525,#7525,#360,.T.);
#5706=EDGE_CURVE('',#7526,#7526,#361,.T.);
#5707=EDGE_CURVE('',#7527,#7527,#362,.T.);
#5708=EDGE_CURVE('',#7528,#7528,#363,.T.);
#5709=EDGE_CURVE('',#7529,#7529,#364,.T.);
#5710=EDGE_CURVE('',#7530,#7530,#365,.T.);
#5711=EDGE_CURVE('',#7531,#7531,#366,.T.);
#5712=EDGE_CURVE('',#7532,#7532,#367,.T.);
#5713=EDGE_CURVE('',#7510,#7515,#368,.T.);
#5714=EDGE_CURVE('',#7502,#7507,#369,.T.);
#5715=EDGE_CURVE('',#7494,#7499,#370,.T.);
#5716=EDGE_CURVE('',#7533,#7533,#371,.T.);
#5717=EDGE_CURVE('',#7534,#7534,#372,.T.);
#5718=EDGE_CURVE('',#7535,#7535,#373,.T.);
#5719=EDGE_CURVE('',#7536,#7536,#374,.T.);
#5720=EDGE_CURVE('',#7537,#7537,#375,.T.);
#5721=EDGE_CURVE('',#7538,#7538,#376,.T.);
#5722=EDGE_CURVE('',#7539,#7539,#377,.T.);
#5723=EDGE_CURVE('',#7540,#7540,#378,.T.);
#5724=EDGE_CURVE('',#7541,#7541,#379,.T.);
#5725=EDGE_CURVE('',#7542,#7542,#380,.T.);
#5726=EDGE_CURVE('',#7509,#7512,#381,.T.);
#5727=EDGE_CURVE('',#7501,#7504,#382,.T.);
#5728=EDGE_CURVE('',#7493,#7496,#383,.T.);
#5729=EDGE_CURVE('',#7543,#7543,#384,.T.);
#5730=EDGE_CURVE('',#7544,#7544,#385,.T.);
#5731=EDGE_CURVE('',#7545,#7545,#386,.T.);
#5732=EDGE_CURVE('',#7546,#7546,#387,.T.);
#5733=EDGE_CURVE('',#7547,#7547,#388,.T.);
#5734=EDGE_CURVE('',#7548,#7548,#389,.T.);
#5735=EDGE_CURVE('',#7487,#7485,#390,.T.);
#7462=VERTEX_POINT('',#19225);
#7463=VERTEX_POINT('',#19226);
#7464=VERTEX_POINT('',#19236);
#7465=VERTEX_POINT('',#19246);
#7466=VERTEX_POINT('',#19256);
#7467=VERTEX_POINT('',#19266);
#7468=VERTEX_POINT('',#19276);
#7469=VERTEX_POINT('',#19286);
#7470=VERTEX_POINT('',#19296);
#7471=VERTEX_POINT('',#19298);
#7472=VERTEX_POINT('',#19358);
#7473=VERTEX_POINT('',#19360);
#7474=VERTEX_POINT('',#19420);
#7475=VERTEX_POINT('',#19540);
#7476=VERTEX_POINT('',#19541);
#7477=VERTEX_POINT('',#19552);
#7478=VERTEX_POINT('',#19562);
#7479=VERTEX_POINT('',#19572);
#7480=VERTEX_POINT('',#19582);
#7481=VERTEX_POINT('',#19592);
#7482=VERTEX_POINT('',#19602);
#7483=VERTEX_POINT('',#19612);
#7484=VERTEX_POINT('',#19616);
#7485=VERTEX_POINT('',#19637);
#7486=VERTEX_POINT('',#19638);
#7487=VERTEX_POINT('',#19640);
#7488=VERTEX_POINT('',#19644);
#7489=VERTEX_POINT('',#19649);
#7490=VERTEX_POINT('',#19652);
#7491=VERTEX_POINT('',#19654);
#7492=VERTEX_POINT('',#19657);
#7493=VERTEX_POINT('',#19658);
#7494=VERTEX_POINT('',#19660);
#7495=VERTEX_POINT('',#19662);
#7496=VERTEX_POINT('',#19666);
#7497=VERTEX_POINT('',#19667);
#7498=VERTEX_POINT('',#19669);
#7499=VERTEX_POINT('',#19671);
#7500=VERTEX_POINT('',#19678);
#7501=VERTEX_POINT('',#19679);
#7502=VERTEX_POINT('',#19681);
#7503=VERTEX_POINT('',#19683);
#7504=VERTEX_POINT('',#19687);
#7505=VERTEX_POINT('',#19688);
#7506=VERTEX_POINT('',#19690);
#7507=VERTEX_POINT('',#19692);
#7508=VERTEX_POINT('',#19699);
#7509=VERTEX_POINT('',#19700);
#7510=VERTEX_POINT('',#19702);
#7511=VERTEX_POINT('',#19704);
#7512=VERTEX_POINT('',#19708);
#7513=VERTEX_POINT('',#19709);
#7514=VERTEX_POINT('',#19711);
#7515=VERTEX_POINT('',#19713);
#7516=VERTEX_POINT('',#19720);
#7517=VERTEX_POINT('',#19722);
#7518=VERTEX_POINT('',#19725);
#7519=VERTEX_POINT('',#19727);
#7520=VERTEX_POINT('',#19730);
#7521=VERTEX_POINT('',#19732);
#7522=VERTEX_POINT('',#19735);
#7523=VERTEX_POINT('',#19737);
#7524=VERTEX_POINT('',#19740);
#7525=VERTEX_POINT('',#19742);
#7526=VERTEX_POINT('',#19744);
#7527=VERTEX_POINT('',#19746);
#7528=VERTEX_POINT('',#19748);
#7529=VERTEX_POINT('',#19750);
#7530=VERTEX_POINT('',#19752);
#7531=VERTEX_POINT('',#19754);
#7532=VERTEX_POINT('',#19756);
#7533=VERTEX_POINT('',#19761);
#7534=VERTEX_POINT('',#19764);
#7535=VERTEX_POINT('',#19766);
#7536=VERTEX_POINT('',#19768);
#7537=VERTEX_POINT('',#19770);
#7538=VERTEX_POINT('',#19772);
#7539=VERTEX_POINT('',#19774);
#7540=VERTEX_POINT('',#19776);
#7541=VERTEX_POINT('',#19778);
#7542=VERTEX_POINT('',#19780);
#7543=VERTEX_POINT('',#19785);
#7544=VERTEX_POINT('',#19788);
#7545=VERTEX_POINT('',#19790);
#7546=VERTEX_POINT('',#19793);
#7547=VERTEX_POINT('',#19795);
#7548=VERTEX_POINT('',#19798);
#8773=LINE('',#19224,#9601);
#8774=LINE('',#19297,#9602);
#8775=LINE('',#19357,#9603);
#8776=LINE('',#19359,#9604);
#8777=LINE('',#19419,#9605);
#8778=LINE('',#19421,#9606);
#8779=LINE('',#19542,#9607);
#8780=LINE('',#19611,#9608);
#8781=LINE('',#19613,#9609);
#8782=LINE('',#19656,#9610);
#8783=LINE('',#19659,#9611);
#8784=LINE('',#19661,#9612);
#8785=LINE('',#19663,#9613);
#8786=LINE('',#19665,#9614);
#8787=LINE('',#19668,#9615);
#8788=LINE('',#19670,#9616);
#8789=LINE('',#19672,#9617);
#8790=LINE('',#19677,#9618);
#8791=LINE('',#19680,#9619);
#8792=LINE('',#19682,#9620);
#8793=LINE('',#19684,#9621);
#8794=LINE('',#19686,#9622);
#8795=LINE('',#19689,#9623);
#8796=LINE('',#19691,#9624);
#8797=LINE('',#19693,#9625);
#8798=LINE('',#19698,#9626);
#8799=LINE('',#19701,#9627);
#8800=LINE('',#19703,#9628);
#8801=LINE('',#19705,#9629);
#8802=LINE('',#19707,#9630);
#8803=LINE('',#19710,#9631);
#8804=LINE('',#19712,#9632);
#8805=LINE('',#19714,#9633);
#9601=VECTOR('',#15297,1.);
#9602=VECTOR('',#15298,1.);
#9603=VECTOR('',#15301,1.);
#9604=VECTOR('',#15302,1.);
#9605=VECTOR('',#15305,1.);
#9606=VECTOR('',#15306,1.);
#9607=VECTOR('',#15307,1.);
#9608=VECTOR('',#15310,1.);
#9609=VECTOR('',#15311,1.);
#9610=VECTOR('',#15336,1.);
#9611=VECTOR('',#15337,1.);
#9612=VECTOR('',#15338,1.);
#9613=VECTOR('',#15339,1.);
#9614=VECTOR('',#15342,1.);
#9615=VECTOR('',#15343,1.);
#9616=VECTOR('',#15344,1.);
#9617=VECTOR('',#15345,1.);
#9618=VECTOR('',#15354,1.);
#9619=VECTOR('',#15355,1.);
#9620=VECTOR('',#15356,1.);
#9621=VECTOR('',#15357,1.);
#9622=VECTOR('',#15360,1.);
#9623=VECTOR('',#15361,1.);
#9624=VECTOR('',#15362,1.);
#9625=VECTOR('',#15363,1.);
#9626=VECTOR('',#15372,1.);
#9627=VECTOR('',#15373,1.);
#9628=VECTOR('',#15374,1.);
#9629=VECTOR('',#15375,1.);
#9630=VECTOR('',#15378,1.);
#9631=VECTOR('',#15379,1.);
#9632=VECTOR('',#15380,1.);
#9633=VECTOR('',#15381,1.);
#10429=EDGE_LOOP('',(#1966,#1967,#1968,#1969,#1970,#1971,#1972,#1973,#1974,
#1975));
#10430=EDGE_LOOP('',(#1976,#1977,#1978,#1979));
#10431=EDGE_LOOP('',(#1980,#1981,#1982,#1983));
#10432=EDGE_LOOP('',(#1984,#1985,#1986,#1987,#1988,#1989,#1990,#1991,#1992,
#1993,#1994));
#10433=EDGE_LOOP('',(#1995,#1996,#1997,#1998,#1999));
#10434=EDGE_LOOP('',(#2000));
#10435=EDGE_LOOP('',(#2001,#2002,#2003));
#10436=EDGE_LOOP('',(#2004,#2005,#2006,#2007));
#10437=EDGE_LOOP('',(#2008,#2009));
#10438=EDGE_LOOP('',(#2010));
#10439=EDGE_LOOP('',(#2011));
#10440=EDGE_LOOP('',(#2012));
#10441=EDGE_LOOP('',(#2013,#2014,#2015,#2016));
#10442=EDGE_LOOP('',(#2017,#2018,#2019,#2020));
#10443=EDGE_LOOP('',(#2021,#2022,#2023,#2024));
#10444=EDGE_LOOP('',(#2025,#2026,#2027,#2028));
#10445=EDGE_LOOP('',(#2029,#2030,#2031,#2032));
#10446=EDGE_LOOP('',(#2033,#2034,#2035,#2036));
#10447=EDGE_LOOP('',(#2037,#2038,#2039,#2040));
#10448=EDGE_LOOP('',(#2041,#2042,#2043,#2044));
#10449=EDGE_LOOP('',(#2045,#2046,#2047,#2048));
#10450=EDGE_LOOP('',(#2049));
#10451=EDGE_LOOP('',(#2050));
#10452=EDGE_LOOP('',(#2051));
#10453=EDGE_LOOP('',(#2052));
#10454=EDGE_LOOP('',(#2053));
#10455=EDGE_LOOP('',(#2054));
#10456=EDGE_LOOP('',(#2055));
#10457=EDGE_LOOP('',(#2056));
#10458=EDGE_LOOP('',(#2057));
#10459=EDGE_LOOP('',(#2058));
#10460=EDGE_LOOP('',(#2059));
#10461=EDGE_LOOP('',(#2060));
#10462=EDGE_LOOP('',(#2061));
#10463=EDGE_LOOP('',(#2062));
#10464=EDGE_LOOP('',(#2063));
#10465=EDGE_LOOP('',(#2064));
#10466=EDGE_LOOP('',(#2065));
#10467=EDGE_LOOP('',(#2066,#2067,#2068,#2069));
#10468=EDGE_LOOP('',(#2070,#2071,#2072,#2073));
#10469=EDGE_LOOP('',(#2074,#2075,#2076,#2077));
#10470=EDGE_LOOP('',(#2078));
#10471=EDGE_LOOP('',(#2079));
#10472=EDGE_LOOP('',(#2080));
#10473=EDGE_LOOP('',(#2081));
#10474=EDGE_LOOP('',(#2082));
#10475=EDGE_LOOP('',(#2083));
#10476=EDGE_LOOP('',(#2084));
#10477=EDGE_LOOP('',(#2085));
#10478=EDGE_LOOP('',(#2086));
#10479=EDGE_LOOP('',(#2087));
#10480=EDGE_LOOP('',(#2088,#2089,#2090,#2091));
#10481=EDGE_LOOP('',(#2092,#2093,#2094,#2095));
#10482=EDGE_LOOP('',(#2096,#2097,#2098,#2099));
#10483=EDGE_LOOP('',(#2100));
#10484=EDGE_LOOP('',(#2101));
#10485=EDGE_LOOP('',(#2102));
#10486=EDGE_LOOP('',(#2103));
#10487=EDGE_LOOP('',(#2104));
#10488=EDGE_LOOP('',(#2105));
#10489=EDGE_LOOP('',(#2106));
#10490=EDGE_LOOP('',(#2107));
#10491=EDGE_LOOP('',(#2108));
#10492=EDGE_LOOP('',(#2109));
#10493=EDGE_LOOP('',(#2110));
#10494=EDGE_LOOP('',(#2111));
#10495=EDGE_LOOP('',(#2112));
#10496=EDGE_LOOP('',(#2113));
#10497=EDGE_LOOP('',(#2114));
#10498=EDGE_LOOP('',(#2115));
#10499=EDGE_LOOP('',(#2116));
#10500=EDGE_LOOP('',(#2117));
#10501=EDGE_LOOP('',(#2118));
#10502=EDGE_LOOP('',(#2119));
#10503=EDGE_LOOP('',(#2120));
#10504=EDGE_LOOP('',(#2121));
#10505=EDGE_LOOP('',(#2122));
#10506=EDGE_LOOP('',(#2123));
#10507=EDGE_LOOP('',(#2124));
#10508=EDGE_LOOP('',(#2125));
#10509=EDGE_LOOP('',(#2126));
#10510=EDGE_LOOP('',(#2127));
#10511=EDGE_LOOP('',(#2128));
#10512=EDGE_LOOP('',(#2129));
#10513=EDGE_LOOP('',(#2130));
#10514=EDGE_LOOP('',(#2131));
#10515=EDGE_LOOP('',(#2132));
#10516=EDGE_LOOP('',(#2133));
#10517=EDGE_LOOP('',(#2134));
#10518=EDGE_LOOP('',(#2135));
#10519=EDGE_LOOP('',(#2136));
#10520=EDGE_LOOP('',(#2137,#2138,#2139,#2140));
#10521=EDGE_LOOP('',(#2141,#2142,#2143,#2144));
#10522=EDGE_LOOP('',(#2145,#2146,#2147,#2148));
#10523=EDGE_LOOP('',(#2149));
#10524=EDGE_LOOP('',(#2150));
#10525=EDGE_LOOP('',(#2151));
#10526=EDGE_LOOP('',(#2152));
#10527=EDGE_LOOP('',(#2153,#2154,#2155,#2156,#2157,#2158,#2159,#2160,#2161,
#2162,#2163,#2164,#2165,#2166,#2167,#2168,#2169));
#10528=EDGE_LOOP('',(#2170,#2171));
#10529=EDGE_LOOP('',(#2172));
#10530=EDGE_LOOP('',(#2173));
#10531=EDGE_LOOP('',(#2174,#2175,#2176,#2177));
#11544=FACE_BOUND('',#10429,.T.);
#11545=FACE_BOUND('',#10430,.T.);
#11546=FACE_BOUND('',#10431,.T.);
#11547=FACE_BOUND('',#10432,.T.);
#11548=FACE_BOUND('',#10433,.T.);
#11549=FACE_BOUND('',#10434,.T.);
#11550=FACE_BOUND('',#10435,.T.);
#11551=FACE_BOUND('',#10436,.T.);
#11552=FACE_BOUND('',#10437,.T.);
#11553=FACE_BOUND('',#10438,.T.);
#11554=FACE_BOUND('',#10439,.T.);
#11555=FACE_BOUND('',#10440,.T.);
#11556=FACE_BOUND('',#10441,.T.);
#11557=FACE_BOUND('',#10442,.T.);
#11558=FACE_BOUND('',#10443,.T.);
#11559=FACE_BOUND('',#10444,.T.);
#11560=FACE_BOUND('',#10445,.T.);
#11561=FACE_BOUND('',#10446,.T.);
#11562=FACE_BOUND('',#10447,.T.);
#11563=FACE_BOUND('',#10448,.T.);
#11564=FACE_BOUND('',#10449,.T.);
#11565=FACE_BOUND('',#10450,.T.);
#11566=FACE_BOUND('',#10451,.T.);
#11567=FACE_BOUND('',#10452,.T.);
#11568=FACE_BOUND('',#10453,.T.);
#11569=FACE_BOUND('',#10454,.T.);
#11570=FACE_BOUND('',#10455,.T.);
#11571=FACE_BOUND('',#10456,.T.);
#11572=FACE_BOUND('',#10457,.T.);
#11573=FACE_BOUND('',#10458,.T.);
#11574=FACE_BOUND('',#10459,.T.);
#11575=FACE_BOUND('',#10460,.T.);
#11576=FACE_BOUND('',#10461,.T.);
#11577=FACE_BOUND('',#10462,.T.);
#11578=FACE_BOUND('',#10463,.T.);
#11579=FACE_BOUND('',#10464,.T.);
#11580=FACE_BOUND('',#10465,.T.);
#11581=FACE_BOUND('',#10466,.T.);
#11582=FACE_BOUND('',#10467,.T.);
#11583=FACE_BOUND('',#10468,.T.);
#11584=FACE_BOUND('',#10469,.T.);
#11585=FACE_BOUND('',#10470,.T.);
#11586=FACE_BOUND('',#10471,.T.);
#11587=FACE_BOUND('',#10472,.T.);
#11588=FACE_BOUND('',#10473,.T.);
#11589=FACE_BOUND('',#10474,.T.);
#11590=FACE_BOUND('',#10475,.T.);
#11591=FACE_BOUND('',#10476,.T.);
#11592=FACE_BOUND('',#10477,.T.);
#11593=FACE_BOUND('',#10478,.T.);
#11594=FACE_BOUND('',#10479,.T.);
#11595=FACE_BOUND('',#10480,.T.);
#11596=FACE_BOUND('',#10481,.T.);
#11597=FACE_BOUND('',#10482,.T.);
#11598=FACE_BOUND('',#10483,.T.);
#11599=FACE_BOUND('',#10484,.T.);
#11600=FACE_BOUND('',#10485,.T.);
#11601=FACE_BOUND('',#10486,.T.);
#11602=FACE_BOUND('',#10487,.T.);
#11603=FACE_BOUND('',#10488,.T.);
#11604=FACE_BOUND('',#10489,.T.);
#11605=FACE_BOUND('',#10490,.T.);
#11606=FACE_BOUND('',#10491,.T.);
#11607=FACE_BOUND('',#10492,.T.);
#11608=FACE_BOUND('',#10493,.T.);
#11609=FACE_BOUND('',#10494,.T.);
#11610=FACE_BOUND('',#10495,.T.);
#11611=FACE_BOUND('',#10496,.T.);
#11612=FACE_BOUND('',#10497,.T.);
#11613=FACE_BOUND('',#10498,.T.);
#11614=FACE_BOUND('',#10499,.T.);
#11615=FACE_BOUND('',#10500,.T.);
#11616=FACE_BOUND('',#10501,.T.);
#11617=FACE_BOUND('',#10502,.T.);
#11618=FACE_BOUND('',#10503,.T.);
#11619=FACE_BOUND('',#10504,.T.);
#11620=FACE_BOUND('',#10505,.T.);
#11621=FACE_BOUND('',#10506,.T.);
#11622=FACE_BOUND('',#10507,.T.);
#11623=FACE_BOUND('',#10508,.T.);
#11624=FACE_BOUND('',#10509,.T.);
#11625=FACE_BOUND('',#10510,.T.);
#11626=FACE_BOUND('',#10511,.T.);
#11627=FACE_BOUND('',#10512,.T.);
#11628=FACE_BOUND('',#10513,.T.);
#11629=FACE_BOUND('',#10514,.T.);
#11630=FACE_BOUND('',#10515,.T.);
#11631=FACE_BOUND('',#10516,.T.);
#11632=FACE_BOUND('',#10517,.T.);
#11633=FACE_BOUND('',#10518,.T.);
#11634=FACE_BOUND('',#10519,.T.);
#11635=FACE_BOUND('',#10520,.T.);
#11636=FACE_BOUND('',#10521,.T.);
#11637=FACE_BOUND('',#10522,.T.);
#11638=FACE_BOUND('',#10523,.T.);
#11639=FACE_BOUND('',#10524,.T.);
#11640=FACE_BOUND('',#10525,.T.);
#11641=FACE_BOUND('',#10526,.T.);
#11642=FACE_BOUND('',#10527,.T.);
#11643=FACE_BOUND('',#10528,.T.);
#11644=FACE_BOUND('',#10529,.T.);
#11645=FACE_BOUND('',#10530,.T.);
#11646=FACE_BOUND('',#10531,.T.);
#12663=(
BOUNDED_SURFACE()
B_SPLINE_SURFACE(1,2,((#19110,#19111,#19112,#19113,#19114,#19115,#19116,
#19117,#19118,#19119,#19120,#19121,#19122,#19123,#19124,#19125,#19126,#19127,
#19128,#19129,#19130,#19131,#19132,#19133,#19134,#19135,#19136,#19137,#19138,
#19139,#19140,#19141,#19142,#19143,#19144,#19145,#19146,#19147,#19148,#19149,
#19150,#19151,#19152,#19153,#19154,#19155,#19156,#19157,#19158,#19159,#19160,
#19161,#19162,#19163,#19164,#19165,#19166),(#19167,#19168,#19169,#19170,
#19171,#19172,#19173,#19174,#19175,#19176,#19177,#19178,#19179,#19180,#19181,
#19182,#19183,#19184,#19185,#19186,#19187,#19188,#19189,#19190,#19191,#19192,
#19193,#19194,#19195,#19196,#19197,#19198,#19199,#19200,#19201,#19202,#19203,
#19204,#19205,#19206,#19207,#19208,#19209,#19210,#19211,#19212,#19213,#19214,
#19215,#19216,#19217,#19218,#19219,#19220,#19221,#19222,#19223)),
 .RULED_SURF.,.F.,.F.,.F.)
B_SPLINE_SURFACE_WITH_KNOTS((2,2),(3,2,2,2,2,2,2,2,2,2,2,2,2,2,2,2,2,2,
2,2,2,2,2,2,2,2,2,2,3),(0.,1.),(0.,0.03125,0.0625,0.09375,0.125,0.15625,
0.1875,0.21875,0.25,0.28125,0.3125,0.34375,0.375,0.40625,0.4375,0.46875,
0.5,0.53125,0.5625,0.59375,0.625,0.65625,0.6875,0.71875,0.75,0.78125,0.8125,
0.84375,0.875),.UNSPECIFIED.)
GEOMETRIC_REPRESENTATION_ITEM()
RATIONAL_B_SPLINE_SURFACE(((1.,0.923879532511287,1.,0.923879532511287,1.,
0.923879532511287,1.,0.923879532511287,1.,0.923879532511287,1.,0.923879532511287,
1.,0.923879532511287,1.,0.923879532511287,1.,0.923879532511287,1.,0.923879532511287,
1.,0.923879532511287,1.,0.923879532511287,1.,0.923879532511287,1.,0.923879532511287,
1.,0.923879532511287,1.,0.923879532511287,1.,0.923879532511287,1.,0.923879532511287,
1.,0.923879532511287,1.,0.923879532511287,1.,0.923879532511287,1.,0.923879532511287,
1.,0.923879532511287,1.,0.923879532511287,1.,0.923879532511287,1.,0.923879532511287,
1.,0.923879532511287,1.,0.923879532511287,1.),(1.,0.923879532511287,1.,
0.923879532511287,1.,0.923879532511287,1.,0.923879532511287,1.,0.923879532511287,
1.,0.923879532511287,1.,0.923879532511287,1.,0.923879532511287,1.,0.923879532511287,
1.,0.923879532511287,1.,0.923879532511287,1.,0.923879532511287,1.,0.923879532511287,
1.,0.923879532511287,1.,0.923879532511287,1.,0.923879532511287,1.,0.923879532511287,
1.,0.923879532511287,1.,0.923879532511287,1.,0.923879532511287,1.,0.923879532511287,
1.,0.923879532511287,1.,0.923879532511287,1.,0.923879532511287,1.,0.923879532511287,
1.,0.923879532511287,1.,0.923879532511287,1.,0.923879532511287,1.)))
REPRESENTATION_ITEM('')
SURFACE()
);
#12664=(
BOUNDED_SURFACE()
B_SPLINE_SURFACE(1,2,((#19422,#19423,#19424,#19425,#19426,#19427,#19428,
#19429,#19430,#19431,#19432,#19433,#19434,#19435,#19436,#19437,#19438,#19439,
#19440,#19441,#19442,#19443,#19444,#19445,#19446,#19447,#19448,#19449,#19450,
#19451,#19452,#19453,#19454,#19455,#19456,#19457,#19458,#19459,#19460,#19461,
#19462,#19463,#19464,#19465,#19466,#19467,#19468,#19469,#19470,#19471,#19472,
#19473,#19474,#19475,#19476,#19477,#19478),(#19479,#19480,#19481,#19482,
#19483,#19484,#19485,#19486,#19487,#19488,#19489,#19490,#19491,#19492,#19493,
#19494,#19495,#19496,#19497,#19498,#19499,#19500,#19501,#19502,#19503,#19504,
#19505,#19506,#19507,#19508,#19509,#19510,#19511,#19512,#19513,#19514,#19515,
#19516,#19517,#19518,#19519,#19520,#19521,#19522,#19523,#19524,#19525,#19526,
#19527,#19528,#19529,#19530,#19531,#19532,#19533,#19534,#19535)),
 .RULED_SURF.,.F.,.F.,.F.)
B_SPLINE_SURFACE_WITH_KNOTS((2,2),(3,2,2,2,2,2,2,2,2,2,2,2,2,2,2,2,2,2,
2,2,2,2,2,2,2,2,2,2,3),(0.,1.),(0.,0.03125,0.0625,0.09375,0.125,0.15625,
0.1875,0.21875,0.25,0.28125,0.3125,0.34375,0.375,0.40625,0.4375,0.46875,
0.5,0.53125,0.5625,0.59375,0.625,0.65625,0.6875,0.71875,0.75,0.78125,0.8125,
0.84375,0.875),.UNSPECIFIED.)
GEOMETRIC_REPRESENTATION_ITEM()
RATIONAL_B_SPLINE_SURFACE(((1.,0.923879532511287,1.,0.923879532511287,1.,
0.923879532511287,1.,0.923879532511287,1.,0.923879532511287,1.,0.923879532511287,
1.,0.923879532511287,1.,0.923879532511287,1.,0.923879532511287,1.,0.923879532511287,
1.,0.923879532511287,1.,0.923879532511287,1.,0.923879532511287,1.,0.923879532511287,
1.,0.923879532511287,1.,0.923879532511287,1.,0.923879532511287,1.,0.923879532511287,
1.,0.923879532511287,1.,0.923879532511287,1.,0.923879532511287,1.,0.923879532511287,
1.,0.923879532511287,1.,0.923879532511287,1.,0.923879532511287,1.,0.923879532511287,
1.,0.923879532511287,1.,0.923879532511287,1.),(1.,0.923879532511287,1.,
0.923879532511287,1.,0.923879532511287,1.,0.923879532511287,1.,0.923879532511287,
1.,0.923879532511287,1.,0.923879532511287,1.,0.923879532511287,1.,0.923879532511287,
1.,0.923879532511287,1.,0.923879532511287,1.,0.923879532511287,1.,0.923879532511287,
1.,0.923879532511287,1.,0.923879532511287,1.,0.923879532511287,1.,0.923879532511287,
1.,0.923879532511287,1.,0.923879532511287,1.,0.923879532511287,1.,0.923879532511287,
1.,0.923879532511287,1.,0.923879532511287,1.,0.923879532511287,1.,0.923879532511287,
1.,0.923879532511287,1.,0.923879532511287,1.,0.923879532511287,1.)))
REPRESENTATION_ITEM('')
SURFACE()
);
#12665=(
BOUNDED_SURFACE()
B_SPLINE_SURFACE(3,3,((#19618,#19619,#19620,#19621),(#19622,#19623,#19624,
#19625),(#19626,#19627,#19628,#19629),(#19630,#19631,#19632,#19633)),
 .SURF_OF_REVOLUTION.,.F.,.F.,.F.)
B_SPLINE_SURFACE_WITH_KNOTS((4,4),(4,4),(0.,1.),(0.,1.),
 .PIECEWISE_BEZIER_KNOTS.)
GEOMETRIC_REPRESENTATION_ITEM()
RATIONAL_B_SPLINE_SURFACE(((1.,0.333333333333333,0.333333333333333,1.),
(1.,0.333333333333333,0.333333333333333,1.),(1.,0.333333333333333,0.333333333333333,
1.),(1.,0.333333333333333,0.333333333333333,1.)))
REPRESENTATION_ITEM('')
SURFACE()
);
#12666=(
BOUNDED_SURFACE()
B_SPLINE_SURFACE(3,3,((#19822,#19823,#19824,#19825),(#19826,#19827,#19828,
#19829),(#19830,#19831,#19832,#19833),(#19834,#19835,#19836,#19837)),
 .SURF_OF_REVOLUTION.,.F.,.F.,.F.)
B_SPLINE_SURFACE_WITH_KNOTS((4,4),(4,4),(0.,1.),(0.,1.),
 .PIECEWISE_BEZIER_KNOTS.)
GEOMETRIC_REPRESENTATION_ITEM()
RATIONAL_B_SPLINE_SURFACE(((1.,0.333333333333333,0.333333333333333,1.),
(1.,0.333333333333333,0.333333333333333,1.),(1.,0.333333333333333,0.333333333333333,
1.),(1.,0.333333333333333,0.333333333333333,1.)))
REPRESENTATION_ITEM('')
SURFACE()
);
#12706=ADVANCED_FACE('',(#11544),#12663,.T.);
#12707=ADVANCED_FACE('',(#11545),#1538,.F.);
#12708=ADVANCED_FACE('',(#11546),#1201,.T.);
#12709=ADVANCED_FACE('',(#11547),#12664,.T.);
#12710=ADVANCED_FACE('',(#11548),#1202,.T.);
#12711=ADVANCED_FACE('',(#11549,#11550),#1203,.F.);
#12712=ADVANCED_FACE('',(#11551),#12665,.F.);
#12713=ADVANCED_FACE('',(#11552,#11553),#1204,.F.);
#12714=ADVANCED_FACE('',(#11554,#11555),#1205,.T.);
#12715=ADVANCED_FACE('',(#11556),#1206,.F.);
#12716=ADVANCED_FACE('',(#11557),#1207,.F.);
#12717=ADVANCED_FACE('',(#11558),#1539,.F.);
#12718=ADVANCED_FACE('',(#11559),#1208,.F.);
#12719=ADVANCED_FACE('',(#11560),#1209,.F.);
#12720=ADVANCED_FACE('',(#11561),#1540,.F.);
#12721=ADVANCED_FACE('',(#11562),#1210,.F.);
#12722=ADVANCED_FACE('',(#11563),#1211,.F.);
#12723=ADVANCED_FACE('',(#11564),#1541,.F.);
#12724=ADVANCED_FACE('',(#11565,#11566),#1212,.F.);
#12725=ADVANCED_FACE('',(#11567,#11568),#1213,.F.);
#12726=ADVANCED_FACE('',(#11569,#11570),#1214,.F.);
#12727=ADVANCED_FACE('',(#11571,#11572),#1215,.F.);
#12728=ADVANCED_FACE('',(#11573,#11574,#11575,#11576,#11577,#11578,#11579,
#11580,#11581,#11582,#11583,#11584,#11585),#1216,.F.);
#12729=ADVANCED_FACE('',(#11586,#11587,#11588,#11589,#11590,#11591,#11592,
#11593,#11594,#11595,#11596,#11597,#11598),#1217,.T.);
#12730=ADVANCED_FACE('',(#11599,#11600),#1218,.T.);
#12731=ADVANCED_FACE('',(#11601,#11602),#1219,.F.);
#12732=ADVANCED_FACE('',(#11603,#11604),#1542,.F.);
#12733=ADVANCED_FACE('',(#11605,#11606),#1543,.F.);
#12734=ADVANCED_FACE('',(#11607,#11608),#1544,.T.);
#12735=ADVANCED_FACE('',(#11609,#11610),#1545,.T.);
#12736=ADVANCED_FACE('',(#11611,#11612),#1546,.T.);
#12737=ADVANCED_FACE('',(#11613,#11614),#1547,.F.);
#12738=ADVANCED_FACE('',(#11615,#11616),#1548,.F.);
#12739=ADVANCED_FACE('',(#11617,#11618),#1549,.F.);
#12740=ADVANCED_FACE('',(#11619,#11620),#1550,.F.);
#12741=ADVANCED_FACE('',(#11621,#11622),#1551,.F.);
#12742=ADVANCED_FACE('',(#11623,#11624),#1552,.F.);
#12743=ADVANCED_FACE('',(#11625,#11626),#1553,.F.);
#12744=ADVANCED_FACE('',(#11627,#11628),#1554,.F.);
#12745=ADVANCED_FACE('',(#11629,#11630),#1555,.F.);
#12746=ADVANCED_FACE('',(#11631,#11632),#1556,.F.);
#12747=ADVANCED_FACE('',(#11633,#11634),#1557,.F.);
#12748=ADVANCED_FACE('',(#11635),#1558,.F.);
#12749=ADVANCED_FACE('',(#11636),#1559,.F.);
#12750=ADVANCED_FACE('',(#11637),#1560,.F.);
#12751=ADVANCED_FACE('',(#11638,#11639),#1561,.F.);
#12752=ADVANCED_FACE('',(#11640,#11641),#1562,.F.);
#12753=ADVANCED_FACE('',(#11642,#11643),#1563,.F.);
#12754=ADVANCED_FACE('',(#11644,#11645),#255,.T.);
#12755=ADVANCED_FACE('',(#11646),#12666,.F.);
#13502=CLOSED_SHELL('',(#12706,#12707,#12708,#12709,#12710,#12711,#12712,
#12713,#12714,#12715,#12716,#12717,#12718,#12719,#12720,#12721,#12722,#12723,
#12724,#12725,#12726,#12727,#12728,#12729,#12730,#12731,#12732,#12733,#12734,
#12735,#12736,#12737,#12738,#12739,#12740,#12741,#12742,#12743,#12744,#12745,
#12746,#12747,#12748,#12749,#12750,#12751,#12752,#12753,#12754,#12755));
#13529=STYLED_ITEM('',(#13556),#13719);
#13556=PRESENTATION_STYLE_ASSIGNMENT((#13583));
#13583=SURFACE_STYLE_USAGE(.BOTH.,#13610);
#13610=SURFACE_SIDE_STYLE('',(#13637));
#13637=SURFACE_STYLE_FILL_AREA(#13664);
#13664=FILL_AREA_STYLE('',(#13691));
#13691=FILL_AREA_STYLE_COLOUR('',#13718);
#13718=COLOUR_RGB('', 0.09019608, 0.27058824, 0.51372549);
#13719=MANIFOLD_SOLID_BREP('Top_acces_nozzle_supporter',#13502);
#13747=SHAPE_DEFINITION_REPRESENTATION(#45524,#13775);
#13775=SHAPE_REPRESENTATION('Top_acces_nozzle_supporter',(#13802),#45465);
#13802=AXIS2_PLACEMENT_3D('',#19109,#15295,#15296);
#13803=AXIS2_PLACEMENT_3D('',#19356,#15299,#15300);
#13804=AXIS2_PLACEMENT_3D('',#19418,#15303,#15304);
#13805=AXIS2_PLACEMENT_3D('',#19610,#15308,#15309);
#13806=AXIS2_PLACEMENT_3D('',#19614,#15312,#15313);
#13807=AXIS2_PLACEMENT_3D('',#19615,#15314,#15315);
#13808=AXIS2_PLACEMENT_3D('',#19617,#15316,#15317);
#13809=AXIS2_PLACEMENT_3D('',#19639,#15318,#15319);
#13810=AXIS2_PLACEMENT_3D('',#19645,#15320,#15321);
#13811=AXIS2_PLACEMENT_3D('',#19646,#15322,#15323);
#13812=AXIS2_PLACEMENT_3D('',#19647,#15324,#15325);
#13813=AXIS2_PLACEMENT_3D('',#19648,#15326,#15327);
#13814=AXIS2_PLACEMENT_3D('',#19650,#15328,#15329);
#13815=AXIS2_PLACEMENT_3D('',#19651,#15330,#15331);
#13816=AXIS2_PLACEMENT_3D('',#19653,#15332,#15333);
#13817=AXIS2_PLACEMENT_3D('',#19655,#15334,#15335);
#13818=AXIS2_PLACEMENT_3D('',#19664,#15340,#15341);
#13819=AXIS2_PLACEMENT_3D('',#19673,#15346,#15347);
#13820=AXIS2_PLACEMENT_3D('',#19674,#15348,#15349);
#13821=AXIS2_PLACEMENT_3D('',#19675,#15350,#15351);
#13822=AXIS2_PLACEMENT_3D('',#19676,#15352,#15353);
#13823=AXIS2_PLACEMENT_3D('',#19685,#15358,#15359);
#13824=AXIS2_PLACEMENT_3D('',#19694,#15364,#15365);
#13825=AXIS2_PLACEMENT_3D('',#19695,#15366,#15367);
#13826=AXIS2_PLACEMENT_3D('',#19696,#15368,#15369);
#13827=AXIS2_PLACEMENT_3D('',#19697,#15370,#15371);
#13828=AXIS2_PLACEMENT_3D('',#19706,#15376,#15377);
#13829=AXIS2_PLACEMENT_3D('',#19715,#15382,#15383);
#13830=AXIS2_PLACEMENT_3D('',#19716,#15384,#15385);
#13831=AXIS2_PLACEMENT_3D('',#19717,#15386,#15387);
#13832=AXIS2_PLACEMENT_3D('',#19718,#15388,#15389);
#13833=AXIS2_PLACEMENT_3D('',#19719,#15390,#15391);
#13834=AXIS2_PLACEMENT_3D('',#19721,#15392,#15393);
#13835=AXIS2_PLACEMENT_3D('',#19723,#15394,#15395);
#13836=AXIS2_PLACEMENT_3D('',#19724,#15396,#15397);
#13837=AXIS2_PLACEMENT_3D('',#19726,#15398,#15399);
#13838=AXIS2_PLACEMENT_3D('',#19728,#15400,#15401);
#13839=AXIS2_PLACEMENT_3D('',#19729,#15402,#15403);
#13840=AXIS2_PLACEMENT_3D('',#19731,#15404,#15405);
#13841=AXIS2_PLACEMENT_3D('',#19733,#15406,#15407);
#13842=AXIS2_PLACEMENT_3D('',#19734,#15408,#15409);
#13843=AXIS2_PLACEMENT_3D('',#19736,#15410,#15411);
#13844=AXIS2_PLACEMENT_3D('',#19738,#15412,#15413);
#13845=AXIS2_PLACEMENT_3D('',#19739,#15414,#15415);
#13846=AXIS2_PLACEMENT_3D('',#19741,#15416,#15417);
#13847=AXIS2_PLACEMENT_3D('',#19743,#15418,#15419);
#13848=AXIS2_PLACEMENT_3D('',#19745,#15420,#15421);
#13849=AXIS2_PLACEMENT_3D('',#19747,#15422,#15423);
#13850=AXIS2_PLACEMENT_3D('',#19749,#15424,#15425);
#13851=AXIS2_PLACEMENT_3D('',#19751,#15426,#15427);
#13852=AXIS2_PLACEMENT_3D('',#19753,#15428,#15429);
#13853=AXIS2_PLACEMENT_3D('',#19755,#15430,#15431);
#13854=AXIS2_PLACEMENT_3D('',#19757,#15432,#15433);
#13855=AXIS2_PLACEMENT_3D('',#19758,#15434,#15435);
#13856=AXIS2_PLACEMENT_3D('',#19759,#15436,#15437);
#13857=AXIS2_PLACEMENT_3D('',#19760,#15438,#15439);
#13858=AXIS2_PLACEMENT_3D('',#19762,#15440,#15441);
#13859=AXIS2_PLACEMENT_3D('',#19763,#15442,#15443);
#13860=AXIS2_PLACEMENT_3D('',#19765,#15444,#15445);
#13861=AXIS2_PLACEMENT_3D('',#19767,#15446,#15447);
#13862=AXIS2_PLACEMENT_3D('',#19769,#15448,#15449);
#13863=AXIS2_PLACEMENT_3D('',#19771,#15450,#15451);
#13864=AXIS2_PLACEMENT_3D('',#19773,#15452,#15453);
#13865=AXIS2_PLACEMENT_3D('',#19775,#15454,#15455);
#13866=AXIS2_PLACEMENT_3D('',#19777,#15456,#15457);
#13867=AXIS2_PLACEMENT_3D('',#19779,#15458,#15459);
#13868=AXIS2_PLACEMENT_3D('',#19781,#15460,#15461);
#13869=AXIS2_PLACEMENT_3D('',#19782,#15462,#15463);
#13870=AXIS2_PLACEMENT_3D('',#19783,#15464,#15465);
#13871=AXIS2_PLACEMENT_3D('',#19784,#15466,#15467);
#13872=AXIS2_PLACEMENT_3D('',#19786,#15468,#15469);
#13873=AXIS2_PLACEMENT_3D('',#19787,#15470,#15471);
#13874=AXIS2_PLACEMENT_3D('',#19789,#15472,#15473);
#13875=AXIS2_PLACEMENT_3D('',#19791,#15474,#15475);
#13876=AXIS2_PLACEMENT_3D('',#19792,#15476,#15477);
#13877=AXIS2_PLACEMENT_3D('',#19794,#15478,#15479);
#13878=AXIS2_PLACEMENT_3D('',#19796,#15480,#15481);
#13879=AXIS2_PLACEMENT_3D('',#19797,#15482,#15483);
#13880=AXIS2_PLACEMENT_3D('',#19799,#15484,#15485);
#13881=AXIS2_PLACEMENT_3D('',#19800,#15486,#15487);
#13882=AXIS2_PLACEMENT_3D('',#19801,#15488,#15489);
#13883=AXIS2_PLACEMENT_3D('',#19802,#15490,#15491);
#13884=AXIS2_PLACEMENT_3D('',#19803,#15492,#15493);
#13885=AXIS2_PLACEMENT_3D('',#19804,#15494,#15495);
#13886=AXIS2_PLACEMENT_3D('',#19805,#15496,#15497);
#13887=AXIS2_PLACEMENT_3D('',#19806,#15498,#15499);
#13888=AXIS2_PLACEMENT_3D('',#19807,#15500,#15501);
#13889=AXIS2_PLACEMENT_3D('',#19808,#15502,#15503);
#13890=AXIS2_PLACEMENT_3D('',#19809,#15504,#15505);
#13891=AXIS2_PLACEMENT_3D('',#19810,#15506,#15507);
#13892=AXIS2_PLACEMENT_3D('',#19811,#15508,#15509);
#13893=AXIS2_PLACEMENT_3D('',#19812,#15510,#15511);
#13894=AXIS2_PLACEMENT_3D('',#19813,#15512,#15513);
#13895=AXIS2_PLACEMENT_3D('',#19814,#15514,#15515);
#13896=AXIS2_PLACEMENT_3D('',#19815,#15516,#15517);
#13897=AXIS2_PLACEMENT_3D('',#19816,#15518,#15519);
#13898=AXIS2_PLACEMENT_3D('',#19817,#15520,#15521);
#13899=AXIS2_PLACEMENT_3D('',#19818,#15522,#15523);
#13900=AXIS2_PLACEMENT_3D('',#19819,#15524,#15525);
#13901=AXIS2_PLACEMENT_3D('',#19820,#15526,#15527);
#13902=AXIS2_PLACEMENT_3D('',#19821,#15528,#15529);
#15295=DIRECTION('',(0.,0.,1.));
#15296=DIRECTION('',(1.,0.,0.));
#15297=DIRECTION('',(0.866025403784438,0.,-0.5));
#15298=DIRECTION('',(0.866025403784438,1.0605752387249E-16,0.5));
#15299=DIRECTION('',(0.,0.,1.));
#15300=DIRECTION('',(1.,0.,0.));
#15301=DIRECTION('',(0.,0.,-1.));
#15302=DIRECTION('',(0.,0.,1.));
#15303=DIRECTION('',(0.,1.,0.));
#15304=DIRECTION('',(-1.,0.,0.));
#15305=DIRECTION('',(0.,0.,-1.));
#15306=DIRECTION('',(-0.866025403784438,-1.0605752387249E-16,0.5));
#15307=DIRECTION('',(-0.866025403784438,0.,-0.5));
#15308=DIRECTION('',(0.,1.,0.));
#15309=DIRECTION('',(-1.,0.,0.));
#15310=DIRECTION('',(0.,0.,1.));
#15311=DIRECTION('',(-1.,0.,0.));
#15312=DIRECTION('',(0.,0.,-1.));
#15313=DIRECTION('',(-1.,0.,0.));
#15314=DIRECTION('',(0.,0.,1.));
#15315=DIRECTION('',(-1.,0.,0.));
#15316=DIRECTION('',(0.,0.,1.));
#15317=DIRECTION('',(1.,0.,0.));
#15318=DIRECTION('',(0.,0.,1.));
#15319=DIRECTION('',(1.,0.,0.));
#15320=DIRECTION('',(0.,0.,1.));
#15321=DIRECTION('',(1.,0.,0.));
#15322=DIRECTION('',(0.,0.,1.));
#15323=DIRECTION('',(1.,0.,0.));
#15324=DIRECTION('',(0.,0.,1.));
#15325=DIRECTION('',(1.,0.,0.));
#15326=DIRECTION('',(0.,0.,-1.));
#15327=DIRECTION('',(1.,0.,0.));
#15328=DIRECTION('',(0.,0.,1.));
#15329=DIRECTION('',(1.,0.,0.));
#15330=DIRECTION('',(0.,0.,-1.));
#15331=DIRECTION('',(1.,0.,0.));
#15332=DIRECTION('',(0.,0.,1.));
#15333=DIRECTION('',(1.,0.,0.));
#15334=DIRECTION('',(0.86602540378444,-0.5,0.));
#15335=DIRECTION('',(0.5,0.86602540378444,0.));
#15336=DIRECTION('',(0.5,0.86602540378444,0.));
#15337=DIRECTION('',(0.,0.,1.));
#15338=DIRECTION('',(0.5,0.86602540378444,0.));
#15339=DIRECTION('',(0.,0.,1.));
#15340=DIRECTION('',(-0.86602540378444,0.5,0.));
#15341=DIRECTION('',(-0.5,-0.86602540378444,0.));
#15342=DIRECTION('',(-0.5,-0.86602540378444,0.));
#15343=DIRECTION('',(0.,0.,1.));
#15344=DIRECTION('',(-0.5,-0.86602540378444,0.));
#15345=DIRECTION('',(0.,0.,1.));
#15346=DIRECTION('',(0.,0.,1.));
#15347=DIRECTION('',(-0.5,0.866025403784436,0.));
#15348=DIRECTION('',(0.,0.,1.));
#15349=DIRECTION('',(-0.5,0.866025403784436,0.));
#15350=DIRECTION('',(0.,0.,1.));
#15351=DIRECTION('',(-0.5,0.866025403784436,0.));
#15352=DIRECTION('',(0.,1.,0.));
#15353=DIRECTION('',(-1.,0.,0.));
#15354=DIRECTION('',(-1.,-6.60582699651968E-15,0.));
#15355=DIRECTION('',(0.,0.,1.));
#15356=DIRECTION('',(-1.,-6.60582699651968E-15,0.));
#15357=DIRECTION('',(0.,0.,1.));
#15358=DIRECTION('',(0.,-1.,0.));
#15359=DIRECTION('',(1.,0.,0.));
#15360=DIRECTION('',(1.,7.105427357601E-15,0.));
#15361=DIRECTION('',(0.,0.,1.));
#15362=DIRECTION('',(1.,7.105427357601E-15,0.));
#15363=DIRECTION('',(0.,0.,1.));
#15364=DIRECTION('',(0.,0.,1.));
#15365=DIRECTION('',(-0.499999999999993,-0.866025403784443,0.));
#15366=DIRECTION('',(0.,0.,1.));
#15367=DIRECTION('',(-0.499999999999993,-0.866025403784443,0.));
#15368=DIRECTION('',(0.,0.,1.));
#15369=DIRECTION('',(-0.499999999999993,-0.866025403784443,0.));
#15370=DIRECTION('',(-0.86602540378444,-0.5,0.));
#15371=DIRECTION('',(0.5,-0.86602540378444,0.));
#15372=DIRECTION('',(0.5,-0.86602540378444,0.));
#15373=DIRECTION('',(0.,0.,1.));
#15374=DIRECTION('',(0.5,-0.86602540378444,0.));
#15375=DIRECTION('',(0.,0.,1.));
#15376=DIRECTION('',(0.86602540378444,0.5,0.));
#15377=DIRECTION('',(-0.5,0.86602540378444,0.));
#15378=DIRECTION('',(-0.5,0.86602540378444,0.));
#15379=DIRECTION('',(0.,0.,1.));
#15380=DIRECTION('',(-0.5,0.86602540378444,0.));
#15381=DIRECTION('',(0.,0.,1.));
#15382=DIRECTION('',(0.,0.,1.));
#15383=DIRECTION('',(1.,0.,0.));
#15384=DIRECTION('',(0.,0.,1.));
#15385=DIRECTION('',(1.,0.,0.));
#15386=DIRECTION('',(0.,0.,1.));
#15387=DIRECTION('',(1.,0.,0.));
#15388=DIRECTION('',(0.,0.,-1.));
#15389=DIRECTION('',(-1.04744440165294E-14,1.,0.));
#15390=DIRECTION('',(0.,0.,1.));
#15391=DIRECTION('',(-3.49148133884314E-15,1.,0.));
#15392=DIRECTION('',(0.,0.,1.));
#15393=DIRECTION('',(-3.49148133884314E-15,1.,0.));
#15394=DIRECTION('',(0.,0.,-1.));
#15395=DIRECTION('',(-1.04744440165294E-14,1.,0.));
#15396=DIRECTION('',(0.,0.,1.));
#15397=DIRECTION('',(-1.,0.,0.));
#15398=DIRECTION('',(0.,0.,1.));
#15399=DIRECTION('',(-1.,0.,0.));
#15400=DIRECTION('',(0.,0.,-1.));
#15401=DIRECTION('',(-1.04744440165294E-14,1.,0.));
#15402=DIRECTION('',(0.,0.,1.));
#15403=DIRECTION('',(1.04744440165294E-14,-1.,0.));
#15404=DIRECTION('',(0.,0.,1.));
#15405=DIRECTION('',(1.04744440165294E-14,-1.,0.));
#15406=DIRECTION('',(0.,0.,-1.));
#15407=DIRECTION('',(-1.04744440165294E-14,1.,0.));
#15408=DIRECTION('',(0.,0.,1.));
#15409=DIRECTION('',(1.,0.,0.));
#15410=DIRECTION('',(0.,0.,1.));
#15411=DIRECTION('',(1.,0.,0.));
#15412=DIRECTION('',(0.,0.,1.));
#15413=DIRECTION('',(1.,0.,0.));
#15414=DIRECTION('',(0.,0.,1.));
#15415=DIRECTION('',(1.,0.,0.));
#15416=DIRECTION('',(0.,0.,1.));
#15417=DIRECTION('',(1.,0.,0.));
#15418=DIRECTION('',(0.,0.,1.));
#15419=DIRECTION('',(1.,0.,0.));
#15420=DIRECTION('',(0.,0.,1.));
#15421=DIRECTION('',(1.,0.,0.));
#15422=DIRECTION('',(0.,0.,1.));
#15423=DIRECTION('',(1.,0.,0.));
#15424=DIRECTION('',(0.,0.,1.));
#15425=DIRECTION('',(1.,0.,0.));
#15426=DIRECTION('',(0.,0.,1.));
#15427=DIRECTION('',(1.04744440165294E-14,-1.,0.));
#15428=DIRECTION('',(0.,0.,1.));
#15429=DIRECTION('',(-1.,0.,0.));
#15430=DIRECTION('',(0.,0.,1.));
#15431=DIRECTION('',(-3.49148133884314E-15,1.,0.));
#15432=DIRECTION('',(0.,0.,1.));
#15433=DIRECTION('',(1.,0.,0.));
#15434=DIRECTION('',(0.,0.,1.));
#15435=DIRECTION('',(-0.499999999999993,-0.866025403784443,0.));
#15436=DIRECTION('',(0.,0.,1.));
#15437=DIRECTION('',(-0.5,0.866025403784436,0.));
#15438=DIRECTION('',(0.,0.,-1.));
#15439=DIRECTION('',(1.,0.,0.));
#15440=DIRECTION('',(0.,0.,1.));
#15441=DIRECTION('',(1.,0.,0.));
#15442=DIRECTION('',(0.,0.,1.));
#15443=DIRECTION('',(1.,0.,0.));
#15444=DIRECTION('',(0.,0.,1.));
#15445=DIRECTION('',(1.,0.,0.));
#15446=DIRECTION('',(0.,0.,1.));
#15447=DIRECTION('',(1.,0.,0.));
#15448=DIRECTION('',(0.,0.,-1.));
#15449=DIRECTION('',(1.,0.,0.));
#15450=DIRECTION('',(0.,0.,1.));
#15451=DIRECTION('',(1.,0.,0.));
#15452=DIRECTION('',(0.,0.,1.));
#15453=DIRECTION('',(1.,0.,0.));
#15454=DIRECTION('',(0.,0.,1.));
#15455=DIRECTION('',(1.04744440165294E-14,-1.,0.));
#15456=DIRECTION('',(0.,0.,1.));
#15457=DIRECTION('',(-1.,0.,0.));
#15458=DIRECTION('',(0.,0.,1.));
#15459=DIRECTION('',(-3.49148133884314E-15,1.,0.));
#15460=DIRECTION('',(0.,0.,1.));
#15461=DIRECTION('',(1.,0.,0.));
#15462=DIRECTION('',(0.,0.,1.));
#15463=DIRECTION('',(-0.499999999999993,-0.866025403784443,0.));
#15464=DIRECTION('',(0.,0.,1.));
#15465=DIRECTION('',(-0.5,0.866025403784436,0.));
#15466=DIRECTION('',(0.,0.,-1.));
#15467=DIRECTION('',(1.,0.,0.));
#15468=DIRECTION('',(0.,0.,1.));
#15469=DIRECTION('',(1.,0.,0.));
#15470=DIRECTION('',(0.,0.,1.));
#15471=DIRECTION('',(1.,0.,0.));
#15472=DIRECTION('',(0.,0.,1.));
#15473=DIRECTION('',(1.,0.,0.));
#15474=DIRECTION('',(0.,0.,1.));
#15475=DIRECTION('',(1.,0.,0.));
#15476=DIRECTION('',(0.,0.,1.));
#15477=DIRECTION('',(1.,0.,0.));
#15478=DIRECTION('',(0.,0.,1.));
#15479=DIRECTION('',(1.,0.,0.));
#15480=DIRECTION('',(0.,0.,1.));
#15481=DIRECTION('',(1.,0.,0.));
#15482=DIRECTION('',(0.,0.,-1.));
#15483=DIRECTION('',(1.,0.,0.));
#15484=DIRECTION('',(0.,0.,1.));
#15485=DIRECTION('',(1.,0.,0.));
#15486=DIRECTION('',(0.,0.,1.));
#15487=DIRECTION('',(1.,0.,0.));
#15488=DIRECTION('',(0.,0.,1.));
#15489=DIRECTION('',(1.,0.,0.));
#15490=DIRECTION('',(0.,0.,-1.));
#15491=DIRECTION('',(-1.,0.,0.));
#15492=DIRECTION('',(0.,0.,-1.));
#15493=DIRECTION('',(-1.,0.,0.));
#15494=DIRECTION('',(0.,0.,-1.));
#15495=DIRECTION('',(-1.,0.,0.));
#15496=DIRECTION('',(0.,0.,-1.));
#15497=DIRECTION('',(-1.,0.,0.));
#15498=DIRECTION('',(0.,0.,1.));
#15499=DIRECTION('',(1.,0.,0.));
#15500=DIRECTION('',(0.,0.,1.));
#15501=DIRECTION('',(1.,0.,0.));
#15502=DIRECTION('',(0.,0.,1.));
#15503=DIRECTION('',(1.04744440165294E-14,-1.,0.));
#15504=DIRECTION('',(0.,0.,1.));
#15505=DIRECTION('',(1.04744440165294E-14,-1.,0.));
#15506=DIRECTION('',(0.,0.,1.));
#15507=DIRECTION('',(-1.,0.,0.));
#15508=DIRECTION('',(0.,0.,1.));
#15509=DIRECTION('',(-1.,0.,0.));
#15510=DIRECTION('',(0.,0.,1.));
#15511=DIRECTION('',(-3.49148133884314E-15,1.,0.));
#15512=DIRECTION('',(0.,0.,1.));
#15513=DIRECTION('',(-3.49148133884314E-15,1.,0.));
#15514=DIRECTION('',(0.,0.,1.));
#15515=DIRECTION('',(1.,0.,0.));
#15516=DIRECTION('',(0.,0.,1.));
#15517=DIRECTION('',(-0.499999999999993,-0.866025403784443,0.));
#15518=DIRECTION('',(0.,0.,1.));
#15519=DIRECTION('',(-0.5,0.866025403784436,0.));
#15520=DIRECTION('',(0.,0.,-1.));
#15521=DIRECTION('',(-1.,0.,0.));
#15522=DIRECTION('',(0.,0.,1.));
#15523=DIRECTION('',(1.,0.,0.));
#15524=DIRECTION('',(0.,0.,1.));
#15525=DIRECTION('',(1.,0.,0.));
#15526=DIRECTION('',(0.,0.,1.));
#15527=DIRECTION('',(1.,0.,0.));
#15528=DIRECTION('',(0.,0.,1.));
#15529=DIRECTION('',(1.,0.,0.));
#19109=CARTESIAN_POINT('',(0.,0.,0.));
#19110=CARTESIAN_POINT('',(-0.00322675153453757,0.,0.100593750002048));
#19111=CARTESIAN_POINT('',(-0.00322675153453757,0.00133656424801366,0.100500000002048));
#19112=CARTESIAN_POINT('',(-0.00228165789127562,0.00228165789127562,0.100406250002048));
#19113=CARTESIAN_POINT('',(-0.00133656424801366,0.00322675153453757,0.100312500002048));
#19114=CARTESIAN_POINT('',(-1.97581546920762E-19,0.00322675153453757,0.100218750002048));
#19115=CARTESIAN_POINT('',(0.00133656424801366,0.00322675153453757,0.100125000002048));
#19116=CARTESIAN_POINT('',(0.00228165789127562,0.00228165789127562,0.100031250002048));
#19117=CARTESIAN_POINT('',(0.00322675153453757,0.00133656424801366,0.0999375000020484));
#19118=CARTESIAN_POINT('',(0.00322675153453757,3.95163093841525E-19,0.0998437500020484));
#19119=CARTESIAN_POINT('',(0.00322675153453757,-0.00133656424801366,0.0997500000020483));
#19120=CARTESIAN_POINT('',(0.00228165789127562,-0.00228165789127562,0.0996562500020484));
#19121=CARTESIAN_POINT('',(0.00133656424801366,-0.00322675153453757,0.0995625000020484));
#19122=CARTESIAN_POINT('',(5.92744640762287E-19,-0.00322675153453757,0.0994687500020484));
#19123=CARTESIAN_POINT('',(-0.00133656424801366,-0.00322675153453757,0.0993750000020484));
#19124=CARTESIAN_POINT('',(-0.00228165789127562,-0.00228165789127562,0.0992812500020484));
#19125=CARTESIAN_POINT('',(-0.00322675153453757,-0.00133656424801366,0.0991875000020485));
#19126=CARTESIAN_POINT('',(-0.00322675153453757,0.,0.0990937500020484));
#19127=CARTESIAN_POINT('',(-0.00322675153453757,0.00133656424801366,0.0990000000020484));
#19128=CARTESIAN_POINT('',(-0.00228165789127562,0.00228165789127562,0.0989062500020484));
#19129=CARTESIAN_POINT('',(-0.00133656424801366,0.00322675153453757,0.0988125000020484));
#19130=CARTESIAN_POINT('',(-1.97581546920762E-19,0.00322675153453757,0.0987187500020484));
#19131=CARTESIAN_POINT('',(0.00133656424801366,0.00322675153453757,0.0986250000020484));
#19132=CARTESIAN_POINT('',(0.00228165789127562,0.00228165789127562,0.0985312500020484));
#19133=CARTESIAN_POINT('',(0.00322675153453757,0.00133656424801366,0.0984375000020484));
#19134=CARTESIAN_POINT('',(0.00322675153453757,3.95163093841525E-19,0.0983437500020484));
#19135=CARTESIAN_POINT('',(0.00322675153453757,-0.00133656424801366,0.0982500000020484));
#19136=CARTESIAN_POINT('',(0.00228165789127562,-0.00228165789127562,0.0981562500020484));
#19137=CARTESIAN_POINT('',(0.00133656424801366,-0.00322675153453757,0.0980625000020485));
#19138=CARTESIAN_POINT('',(5.92744640762287E-19,-0.00322675153453757,0.0979687500020484));
#19139=CARTESIAN_POINT('',(-0.00133656424801366,-0.00322675153453757,0.0978750000020484));
#19140=CARTESIAN_POINT('',(-0.00228165789127562,-0.00228165789127562,0.0977812500020484));
#19141=CARTESIAN_POINT('',(-0.00322675153453757,-0.00133656424801366,0.0976875000020484));
#19142=CARTESIAN_POINT('',(-0.00322675153453757,0.,0.0975937500020484));
#19143=CARTESIAN_POINT('',(-0.00322675153453757,0.00133656424801366,0.0975000000020484));
#19144=CARTESIAN_POINT('',(-0.00228165789127562,0.00228165789127562,0.0974062500020484));
#19145=CARTESIAN_POINT('',(-0.00133656424801366,0.00322675153453757,0.0973125000020484));
#19146=CARTESIAN_POINT('',(-1.97581546920762E-19,0.00322675153453757,0.0972187500020484));
#19147=CARTESIAN_POINT('',(0.00133656424801366,0.00322675153453757,0.0971250000020484));
#19148=CARTESIAN_POINT('',(0.00228165789127562,0.00228165789127562,0.0970312500020484));
#19149=CARTESIAN_POINT('',(0.00322675153453757,0.00133656424801366,0.0969375000020484));
#19150=CARTESIAN_POINT('',(0.00322675153453757,3.95163093841525E-19,0.0968437500020484));
#19151=CARTESIAN_POINT('',(0.00322675153453757,-0.00133656424801366,0.0967500000020484));
#19152=CARTESIAN_POINT('',(0.00228165789127562,-0.00228165789127562,0.0966562500020484));
#19153=CARTESIAN_POINT('',(0.00133656424801366,-0.00322675153453757,0.0965625000020484));
#19154=CARTESIAN_POINT('',(5.92744640762287E-19,-0.00322675153453757,0.0964687500020484));
#19155=CARTESIAN_POINT('',(-0.00133656424801366,-0.00322675153453757,0.0963750000020484));
#19156=CARTESIAN_POINT('',(-0.00228165789127562,-0.00228165789127562,0.0962812500020484));
#19157=CARTESIAN_POINT('',(-0.00322675153453757,-0.00133656424801366,0.0961875000020484));
#19158=CARTESIAN_POINT('',(-0.00322675153453757,0.,0.0960937500020484));
#19159=CARTESIAN_POINT('',(-0.00322675153453757,0.00133656424801366,0.0960000000020484));
#19160=CARTESIAN_POINT('',(-0.00228165789127562,0.00228165789127562,0.0959062500020484));
#19161=CARTESIAN_POINT('',(-0.00133656424801366,0.00322675153453757,0.0958125000020485));
#19162=CARTESIAN_POINT('',(-1.97581546920762E-19,0.00322675153453757,0.0957187500020484));
#19163=CARTESIAN_POINT('',(0.00133656424801366,0.00322675153453757,0.0956250000020484));
#19164=CARTESIAN_POINT('',(0.00228165789127562,0.00228165789127562,0.0955312500020484));
#19165=CARTESIAN_POINT('',(0.00322675153453757,0.00133656424801366,0.0954375000020484));
#19166=CARTESIAN_POINT('',(0.00322675153453757,3.95163093841525E-19,0.0953437500020484));
#19167=CARTESIAN_POINT('',(-0.00241485272203757,0.,0.100125000004097));
#19168=CARTESIAN_POINT('',(-0.00241485272203757,0.00100026474860155,0.100031250004097));
#19169=CARTESIAN_POINT('',(-0.00170755873531956,0.00170755873531956,0.0999375000040968));
#19170=CARTESIAN_POINT('',(-0.00100026474860155,0.00241485272203757,0.0998437500040967));
#19171=CARTESIAN_POINT('',(-1.47867082822779E-19,0.00241485272203757,0.0997500000040968));
#19172=CARTESIAN_POINT('',(0.00100026474860155,0.00241485272203757,0.0996562500040968));
#19173=CARTESIAN_POINT('',(0.00170755873531956,0.00170755873531956,0.0995625000040968));
#19174=CARTESIAN_POINT('',(0.00241485272203757,0.00100026474860155,0.0994687500040968));
#19175=CARTESIAN_POINT('',(0.00241485272203757,2.95734165645558E-19,0.0993750000040968));
#19176=CARTESIAN_POINT('',(0.00241485272203757,-0.00100026474860155,0.0992812500040967));
#19177=CARTESIAN_POINT('',(0.00170755873531956,-0.00170755873531956,0.0991875000040968));
#19178=CARTESIAN_POINT('',(0.00100026474860155,-0.00241485272203757,0.0990937500040968));
#19179=CARTESIAN_POINT('',(4.43601248468338E-19,-0.00241485272203757,0.0990000000040968));
#19180=CARTESIAN_POINT('',(-0.00100026474860155,-0.00241485272203757,0.0989062500040968));
#19181=CARTESIAN_POINT('',(-0.00170755873531956,-0.00170755873531956,0.0988125000040968));
#19182=CARTESIAN_POINT('',(-0.00241485272203757,-0.00100026474860155,0.0987187500040969));
#19183=CARTESIAN_POINT('',(-0.00241485272203757,0.,0.0986250000040968));
#19184=CARTESIAN_POINT('',(-0.00241485272203757,0.00100026474860155,0.0985312500040968));
#19185=CARTESIAN_POINT('',(-0.00170755873531956,0.00170755873531956,0.0984375000040968));
#19186=CARTESIAN_POINT('',(-0.00100026474860155,0.00241485272203757,0.0983437500040968));
#19187=CARTESIAN_POINT('',(-1.47867082822779E-19,0.00241485272203757,0.0982500000040968));
#19188=CARTESIAN_POINT('',(0.00100026474860155,0.00241485272203757,0.0981562500040967));
#19189=CARTESIAN_POINT('',(0.00170755873531956,0.00170755873531956,0.0980625000040968));
#19190=CARTESIAN_POINT('',(0.00241485272203757,0.00100026474860155,0.0979687500040968));
#19191=CARTESIAN_POINT('',(0.00241485272203757,2.95734165645558E-19,0.0978750000040968));
#19192=CARTESIAN_POINT('',(0.00241485272203757,-0.00100026474860155,0.0977812500040968));
#19193=CARTESIAN_POINT('',(0.00170755873531956,-0.00170755873531956,0.0976875000040968));
#19194=CARTESIAN_POINT('',(0.00100026474860155,-0.00241485272203757,0.0975937500040969));
#19195=CARTESIAN_POINT('',(4.43601248468338E-19,-0.00241485272203757,0.0975000000040968));
#19196=CARTESIAN_POINT('',(-0.00100026474860155,-0.00241485272203757,0.0974062500040968));
#19197=CARTESIAN_POINT('',(-0.00170755873531956,-0.00170755873531956,0.0973125000040968));
#19198=CARTESIAN_POINT('',(-0.00241485272203757,-0.00100026474860155,0.0972187500040968));
#19199=CARTESIAN_POINT('',(-0.00241485272203757,0.,0.0971250000040968));
#19200=CARTESIAN_POINT('',(-0.00241485272203757,0.00100026474860155,0.0970312500040968));
#19201=CARTESIAN_POINT('',(-0.00170755873531956,0.00170755873531956,0.0969375000040968));
#19202=CARTESIAN_POINT('',(-0.00100026474860155,0.00241485272203757,0.0968437500040968));
#19203=CARTESIAN_POINT('',(-1.47867082822779E-19,0.00241485272203757,0.0967500000040968));
#19204=CARTESIAN_POINT('',(0.00100026474860155,0.00241485272203757,0.0966562500040968));
#19205=CARTESIAN_POINT('',(0.00170755873531956,0.00170755873531956,0.0965625000040968));
#19206=CARTESIAN_POINT('',(0.00241485272203757,0.00100026474860155,0.0964687500040968));
#19207=CARTESIAN_POINT('',(0.00241485272203757,2.95734165645558E-19,0.0963750000040968));
#19208=CARTESIAN_POINT('',(0.00241485272203757,-0.00100026474860155,0.0962812500040968));
#19209=CARTESIAN_POINT('',(0.00170755873531956,-0.00170755873531956,0.0961875000040968));
#19210=CARTESIAN_POINT('',(0.00100026474860155,-0.00241485272203757,0.0960937500040968));
#19211=CARTESIAN_POINT('',(4.43601248468338E-19,-0.00241485272203757,0.0960000000040968));
#19212=CARTESIAN_POINT('',(-0.00100026474860155,-0.00241485272203757,0.0959062500040968));
#19213=CARTESIAN_POINT('',(-0.00170755873531956,-0.00170755873531956,0.0958125000040968));
#19214=CARTESIAN_POINT('',(-0.00241485272203757,-0.00100026474860155,0.0957187500040968));
#19215=CARTESIAN_POINT('',(-0.00241485272203757,0.,0.0956250000040968));
#19216=CARTESIAN_POINT('',(-0.00241485272203757,0.00100026474860155,0.0955312500040968));
#19217=CARTESIAN_POINT('',(-0.00170755873531956,0.00170755873531956,0.0954375000040968));
#19218=CARTESIAN_POINT('',(-0.00100026474860155,0.00241485272203757,0.0953437500040968));
#19219=CARTESIAN_POINT('',(-1.47867082822779E-19,0.00241485272203757,0.0952500000040968));
#19220=CARTESIAN_POINT('',(0.00100026474860155,0.00241485272203757,0.0951562500040968));
#19221=CARTESIAN_POINT('',(0.00170755873531956,0.00170755873531956,0.0950625000040968));
#19222=CARTESIAN_POINT('',(0.00241485272203757,0.00100026474860155,0.0949687500040968));
#19223=CARTESIAN_POINT('',(0.00241485272203757,2.95734165645558E-19,0.0948750000040968));
#19224=CARTESIAN_POINT('',(-0.00282080212828757,0.,0.100359375003073));
#19225=CARTESIAN_POINT('',(-0.00322675153453757,0.,0.100593750002048));
#19226=CARTESIAN_POINT('',(-0.00241485272203757,0.,0.100125000004097));
#19227=CARTESIAN_POINT('',(-0.00241485272203757,0.,0.100125000004097));
#19228=CARTESIAN_POINT('',(-0.00241485272203757,0.00100026474860155,0.100031250004097));
#19229=CARTESIAN_POINT('',(-0.00170755873531956,0.00170755873531956,0.0999375000040968));
#19230=CARTESIAN_POINT('',(-0.00100026474860155,0.00241485272203757,0.0998437500040967));
#19231=CARTESIAN_POINT('',(-1.47867082822779E-19,0.00241485272203757,0.0997500000040968));
#19232=CARTESIAN_POINT('',(0.00100026474860155,0.00241485272203757,0.0996562500040968));
#19233=CARTESIAN_POINT('',(0.00170755873531956,0.00170755873531956,0.0995625000040968));
#19234=CARTESIAN_POINT('',(0.00241485272203757,0.00100026474860155,0.0994687500040968));
#19235=CARTESIAN_POINT('',(0.00241485272203757,2.95734165645558E-19,0.0993750000040968));
#19236=CARTESIAN_POINT('',(0.00241485272203757,2.95734165645558E-19,0.0993750000040968));
#19237=CARTESIAN_POINT('',(0.00241485272203757,2.95734165645558E-19,0.0993750000040968));
#19238=CARTESIAN_POINT('',(0.00241485272203757,-0.00100026474860155,0.0992812500040967));
#19239=CARTESIAN_POINT('',(0.00170755873531956,-0.00170755873531956,0.0991875000040968));
#19240=CARTESIAN_POINT('',(0.00100026474860155,-0.00241485272203757,0.0990937500040968));
#19241=CARTESIAN_POINT('',(4.43601248468338E-19,-0.00241485272203757,0.0990000000040968));
#19242=CARTESIAN_POINT('',(-0.00100026474860155,-0.00241485272203757,0.0989062500040968));
#19243=CARTESIAN_POINT('',(-0.00170755873531956,-0.00170755873531956,0.0988125000040968));
#19244=CARTESIAN_POINT('',(-0.00241485272203757,-0.00100026474860155,0.0987187500040969));
#19245=CARTESIAN_POINT('',(-0.00241485272203757,0.,0.0986250000040968));
#19246=CARTESIAN_POINT('',(-0.00241485272203757,0.,0.0986250000040968));
#19247=CARTESIAN_POINT('',(-0.00241485272203757,0.,0.0986250000040968));
#19248=CARTESIAN_POINT('',(-0.00241485272203757,0.00100026474860155,0.0985312500040968));
#19249=CARTESIAN_POINT('',(-0.00170755873531956,0.00170755873531956,0.0984375000040968));
#19250=CARTESIAN_POINT('',(-0.00100026474860155,0.00241485272203757,0.0983437500040968));
#19251=CARTESIAN_POINT('',(-1.47867082822779E-19,0.00241485272203757,0.0982500000040968));
#19252=CARTESIAN_POINT('',(0.00100026474860155,0.00241485272203757,0.0981562500040967));
#19253=CARTESIAN_POINT('',(0.00170755873531956,0.00170755873531956,0.0980625000040968));
#19254=CARTESIAN_POINT('',(0.00241485272203757,0.00100026474860155,0.0979687500040968));
#19255=CARTESIAN_POINT('',(0.00241485272203757,2.95734165645558E-19,0.0978750000040968));
#19256=CARTESIAN_POINT('',(0.00241485272203757,2.95734165645558E-19,0.0978750000040968));
#19257=CARTESIAN_POINT('',(0.00241485272203757,2.95734165645558E-19,0.0978750000040968));
#19258=CARTESIAN_POINT('',(0.00241485272203757,-0.00100026474860154,0.0977812500040968));
#19259=CARTESIAN_POINT('',(0.00170755873531956,-0.00170755873531956,0.0976875000040968));
#19260=CARTESIAN_POINT('',(0.00100026474860155,-0.00241485272203757,0.0975937500040969));
#19261=CARTESIAN_POINT('',(4.43601248468338E-19,-0.00241485272203757,0.0975000000040968));
#19262=CARTESIAN_POINT('',(-0.00100026474860155,-0.00241485272203757,0.0974062500040968));
#19263=CARTESIAN_POINT('',(-0.00170755873531956,-0.00170755873531956,0.0973125000040968));
#19264=CARTESIAN_POINT('',(-0.00241485272203757,-0.00100026474860155,0.0972187500040968));
#19265=CARTESIAN_POINT('',(-0.00241485272203757,0.,0.0971250000040968));
#19266=CARTESIAN_POINT('',(-0.00241485272203757,0.,0.0971250000040968));
#19267=CARTESIAN_POINT('',(-0.00241485272203757,0.,0.0971250000040968));
#19268=CARTESIAN_POINT('',(-0.00241485272203757,0.00100026474860155,0.0970312500040967));
#19269=CARTESIAN_POINT('',(-0.00170755873531956,0.00170755873531956,0.0969375000040968));
#19270=CARTESIAN_POINT('',(-0.00100026474860155,0.00241485272203757,0.0968437500040968));
#19271=CARTESIAN_POINT('',(-1.47867082822779E-19,0.00241485272203757,0.0967500000040968));
#19272=CARTESIAN_POINT('',(0.00100026474860155,0.00241485272203757,0.0966562500040968));
#19273=CARTESIAN_POINT('',(0.00170755873531956,0.00170755873531956,0.0965625000040968));
#19274=CARTESIAN_POINT('',(0.00241485272203757,0.00100026474860155,0.0964687500040968));
#19275=CARTESIAN_POINT('',(0.00241485272203757,2.95734165645558E-19,0.0963750000040968));
#19276=CARTESIAN_POINT('',(0.00241485272203757,2.95734165645558E-19,0.0963750000040968));
#19277=CARTESIAN_POINT('',(0.00241485272203757,2.95734165645558E-19,0.0963750000040968));
#19278=CARTESIAN_POINT('',(0.00241485272203757,-0.00100026474860155,0.0962812500040968));
#19279=CARTESIAN_POINT('',(0.00170755873531956,-0.00170755873531956,0.0961875000040968));
#19280=CARTESIAN_POINT('',(0.00100026474860155,-0.00241485272203757,0.0960937500040968));
#19281=CARTESIAN_POINT('',(4.43601248468338E-19,-0.00241485272203757,0.0960000000040968));
#19282=CARTESIAN_POINT('',(-0.00100026474860155,-0.00241485272203757,0.0959062500040968));
#19283=CARTESIAN_POINT('',(-0.00170755873531956,-0.00170755873531956,0.0958125000040968));
#19284=CARTESIAN_POINT('',(-0.00241485272203757,-0.00100026474860155,0.0957187500040968));
#19285=CARTESIAN_POINT('',(-0.00241485272203757,0.,0.0956250000040968));
#19286=CARTESIAN_POINT('',(-0.00241485272203757,0.,0.0956250000040968));
#19287=CARTESIAN_POINT('',(-0.00241485272203757,0.,0.0956250000040968));
#19288=CARTESIAN_POINT('',(-0.00241485272203757,0.00100026474860155,0.0955312500040968));
#19289=CARTESIAN_POINT('',(-0.00170755873531956,0.00170755873531956,0.0954375000040968));
#19290=CARTESIAN_POINT('',(-0.00100026474860155,0.00241485272203757,0.0953437500040968));
#19291=CARTESIAN_POINT('',(-1.47867082822779E-19,0.00241485272203757,0.0952500000040968));
#19292=CARTESIAN_POINT('',(0.00100026474860155,0.00241485272203757,0.0951562500040968));
#19293=CARTESIAN_POINT('',(0.00170755873531956,0.00170755873531956,0.0950625000040968));
#19294=CARTESIAN_POINT('',(0.00241485272203757,0.00100026474860155,0.0949687500040968));
#19295=CARTESIAN_POINT('',(0.00241485272203757,2.95734165645558E-19,0.0948750000040968));
#19296=CARTESIAN_POINT('',(0.00241485272203757,2.21800624234168E-19,0.0948750000040968));
#19297=CARTESIAN_POINT('',(0.00282080212828757,3.45448629743542E-19,0.0951093750030726));
#19298=CARTESIAN_POINT('',(0.00322675153453757,3.95163093841525E-19,0.0953437500020484));
#19299=CARTESIAN_POINT('',(-0.00322675153453757,0.,0.100593750002048));
#19300=CARTESIAN_POINT('',(-0.00322675153453757,0.00133656424801366,0.100500000002048));
#19301=CARTESIAN_POINT('',(-0.00228165789127562,0.00228165789127562,0.100406250002048));
#19302=CARTESIAN_POINT('',(-0.00133656424801366,0.00322675153453757,0.100312500002048));
#19303=CARTESIAN_POINT('',(-1.97581546920762E-19,0.00322675153453757,0.100218750002048));
#19304=CARTESIAN_POINT('',(0.00133656424801366,0.00322675153453757,0.100125000002048));
#19305=CARTESIAN_POINT('',(0.00228165789127562,0.00228165789127562,0.100031250002048));
#19306=CARTESIAN_POINT('',(0.00322675153453757,0.00133656424801366,0.0999375000020484));
#19307=CARTESIAN_POINT('',(0.00322675153453757,3.95163093841525E-19,0.0998437500020484));
#19308=CARTESIAN_POINT('',(0.00322675153453757,-0.00133656424801366,0.0997500000020483));
#19309=CARTESIAN_POINT('',(0.00228165789127562,-0.00228165789127562,0.0996562500020484));
#19310=CARTESIAN_POINT('',(0.00133656424801366,-0.00322675153453757,0.0995625000020484));
#19311=CARTESIAN_POINT('',(5.92744640762287E-19,-0.00322675153453757,0.0994687500020484));
#19312=CARTESIAN_POINT('',(-0.00133656424801366,-0.00322675153453757,0.0993750000020484));
#19313=CARTESIAN_POINT('',(-0.00228165789127562,-0.00228165789127562,0.0992812500020484));
#19314=CARTESIAN_POINT('',(-0.00322675153453757,-0.00133656424801366,0.0991875000020485));
#19315=CARTESIAN_POINT('',(-0.00322675153453757,0.,0.0990937500020484));
#19316=CARTESIAN_POINT('',(-0.00322675153453757,0.00133656424801366,0.0990000000020484));
#19317=CARTESIAN_POINT('',(-0.00228165789127562,0.00228165789127562,0.0989062500020484));
#19318=CARTESIAN_POINT('',(-0.00133656424801366,0.00322675153453757,0.0988125000020484));
#19319=CARTESIAN_POINT('',(-1.97581546920762E-19,0.00322675153453757,0.0987187500020484));
#19320=CARTESIAN_POINT('',(0.00133656424801366,0.00322675153453757,0.0986250000020484));
#19321=CARTESIAN_POINT('',(0.00228165789127562,0.00228165789127562,0.0985312500020484));
#19322=CARTESIAN_POINT('',(0.00322675153453757,0.00133656424801366,0.0984375000020484));
#19323=CARTESIAN_POINT('',(0.00322675153453757,3.95163093841525E-19,0.0983437500020484));
#19324=CARTESIAN_POINT('',(0.00322675153453757,-0.00133656424801366,0.0982500000020484));
#19325=CARTESIAN_POINT('',(0.00228165789127562,-0.00228165789127562,0.0981562500020484));
#19326=CARTESIAN_POINT('',(0.00133656424801366,-0.00322675153453757,0.0980625000020485));
#19327=CARTESIAN_POINT('',(5.92744640762287E-19,-0.00322675153453757,0.0979687500020484));
#19328=CARTESIAN_POINT('',(-0.00133656424801366,-0.00322675153453757,0.0978750000020484));
#19329=CARTESIAN_POINT('',(-0.00228165789127562,-0.00228165789127562,0.0977812500020484));
#19330=CARTESIAN_POINT('',(-0.00322675153453757,-0.00133656424801366,0.0976875000020484));
#19331=CARTESIAN_POINT('',(-0.00322675153453757,0.,0.0975937500020484));
#19332=CARTESIAN_POINT('',(-0.00322675153453757,0.00133656424801366,0.0975000000020484));
#19333=CARTESIAN_POINT('',(-0.00228165789127562,0.00228165789127562,0.0974062500020484));
#19334=CARTESIAN_POINT('',(-0.00133656424801366,0.00322675153453757,0.0973125000020484));
#19335=CARTESIAN_POINT('',(-1.97581546920762E-19,0.00322675153453757,0.0972187500020484));
#19336=CARTESIAN_POINT('',(0.00133656424801366,0.00322675153453757,0.0971250000020484));
#19337=CARTESIAN_POINT('',(0.00228165789127562,0.00228165789127562,0.0970312500020484));
#19338=CARTESIAN_POINT('',(0.00322675153453757,0.00133656424801366,0.0969375000020483));
#19339=CARTESIAN_POINT('',(0.00322675153453757,3.95163093841525E-19,0.0968437500020484));
#19340=CARTESIAN_POINT('',(0.00322675153453757,-0.00133656424801366,0.0967500000020484));
#19341=CARTESIAN_POINT('',(0.00228165789127562,-0.00228165789127562,0.0966562500020484));
#19342=CARTESIAN_POINT('',(0.00133656424801366,-0.00322675153453757,0.0965625000020484));
#19343=CARTESIAN_POINT('',(5.92744640762287E-19,-0.00322675153453757,0.0964687500020484));
#19344=CARTESIAN_POINT('',(-0.00133656424801366,-0.00322675153453757,0.0963750000020484));
#19345=CARTESIAN_POINT('',(-0.00228165789127562,-0.00228165789127562,0.0962812500020484));
#19346=CARTESIAN_POINT('',(-0.00322675153453757,-0.00133656424801366,0.0961875000020484));
#19347=CARTESIAN_POINT('',(-0.00322675153453757,0.,0.0960937500020484));
#19348=CARTESIAN_POINT('',(-0.00322675153453757,0.00133656424801366,0.0960000000020484));
#19349=CARTESIAN_POINT('',(-0.00228165789127562,0.00228165789127562,0.0959062500020484));
#19350=CARTESIAN_POINT('',(-0.00133656424801366,0.00322675153453757,0.0958125000020485));
#19351=CARTESIAN_POINT('',(-1.97581546920762E-19,0.00322675153453757,0.0957187500020484));
#19352=CARTESIAN_POINT('',(0.00133656424801366,0.00322675153453757,0.0956250000020484));
#19353=CARTESIAN_POINT('',(0.00228165789127562,0.00228165789127562,0.0955312500020484));
#19354=CARTESIAN_POINT('',(0.00322675153453757,0.00133656424801366,0.0954375000020484));
#19355=CARTESIAN_POINT('',(0.00322675153453757,3.95163093841525E-19,0.0953437500020484));
#19356=CARTESIAN_POINT('',(1.0842021724855E-18,-4.33680868994202E-18,0.0996930389370738));
#19357=CARTESIAN_POINT('',(-0.00322675153453757,0.,0.100687500002048));
#19358=CARTESIAN_POINT('',(-0.00322675153453757,0.,0.100781250002048));
#19359=CARTESIAN_POINT('',(0.00322675153453757,3.95163093841525E-19,0.0954375000020484));
#19360=CARTESIAN_POINT('',(0.00322675153453757,3.95163093841525E-19,0.0955312500020484));
#19361=CARTESIAN_POINT('',(-0.00322675153453757,0.,0.100781250002048));
#19362=CARTESIAN_POINT('',(-0.00322675153453757,0.00133656424801366,0.100687500002048));
#19363=CARTESIAN_POINT('',(-0.00228165789127562,0.00228165789127562,0.100593750002048));
#19364=CARTESIAN_POINT('',(-0.00133656424801366,0.00322675153453757,0.100500000002048));
#19365=CARTESIAN_POINT('',(-1.97581546920762E-19,0.00322675153453757,0.100406250002048));
#19366=CARTESIAN_POINT('',(0.00133656424801366,0.00322675153453757,0.100312500002048));
#19367=CARTESIAN_POINT('',(0.00228165789127562,0.00228165789127562,0.100218750002048));
#19368=CARTESIAN_POINT('',(0.00322675153453757,0.00133656424801366,0.100125000002048));
#19369=CARTESIAN_POINT('',(0.00322675153453757,3.95163093841525E-19,0.100031250002048));
#19370=CARTESIAN_POINT('',(0.00322675153453757,-0.00133656424801366,0.0999375000020484));
#19371=CARTESIAN_POINT('',(0.00228165789127562,-0.00228165789127562,0.0998437500020484));
#19372=CARTESIAN_POINT('',(0.00133656424801366,-0.00322675153453757,0.0997500000020483));
#19373=CARTESIAN_POINT('',(5.92744640762287E-19,-0.00322675153453757,0.0996562500020484));
#19374=CARTESIAN_POINT('',(-0.00133656424801366,-0.00322675153453757,0.0995625000020484));
#19375=CARTESIAN_POINT('',(-0.00228165789127562,-0.00228165789127562,0.0994687500020484));
#19376=CARTESIAN_POINT('',(-0.00322675153453757,-0.00133656424801366,0.0993750000020484));
#19377=CARTESIAN_POINT('',(-0.00322675153453757,0.,0.0992812500020484));
#19378=CARTESIAN_POINT('',(-0.00322675153453757,0.00133656424801366,0.0991875000020483));
#19379=CARTESIAN_POINT('',(-0.00228165789127562,0.00228165789127562,0.0990937500020484));
#19380=CARTESIAN_POINT('',(-0.00133656424801366,0.00322675153453757,0.0990000000020484));
#19381=CARTESIAN_POINT('',(-1.97581546920762E-19,0.00322675153453757,0.0989062500020484));
#19382=CARTESIAN_POINT('',(0.00133656424801366,0.00322675153453757,0.0988125000020484));
#19383=CARTESIAN_POINT('',(0.00228165789127562,0.00228165789127562,0.0987187500020484));
#19384=CARTESIAN_POINT('',(0.00322675153453757,0.00133656424801366,0.0986250000020484));
#19385=CARTESIAN_POINT('',(0.00322675153453757,3.95163093841525E-19,0.0985312500020484));
#19386=CARTESIAN_POINT('',(0.00322675153453757,-0.00133656424801366,0.0984375000020484));
#19387=CARTESIAN_POINT('',(0.00228165789127562,-0.00228165789127562,0.0983437500020484));
#19388=CARTESIAN_POINT('',(0.00133656424801366,-0.00322675153453757,0.0982500000020484));
#19389=CARTESIAN_POINT('',(5.92744640762287E-19,-0.00322675153453757,0.0981562500020484));
#19390=CARTESIAN_POINT('',(-0.00133656424801366,-0.00322675153453757,0.0980625000020483));
#19391=CARTESIAN_POINT('',(-0.00228165789127562,-0.00228165789127562,0.0979687500020484));
#19392=CARTESIAN_POINT('',(-0.00322675153453757,-0.00133656424801366,0.0978750000020484));
#19393=CARTESIAN_POINT('',(-0.00322675153453757,0.,0.0977812500020484));
#19394=CARTESIAN_POINT('',(-0.00322675153453757,0.00133656424801366,0.0976875000020484));
#19395=CARTESIAN_POINT('',(-0.00228165789127562,0.00228165789127562,0.0975937500020484));
#19396=CARTESIAN_POINT('',(-0.00133656424801366,0.00322675153453757,0.0975000000020484));
#19397=CARTESIAN_POINT('',(-1.97581546920762E-19,0.00322675153453757,0.0974062500020484));
#19398=CARTESIAN_POINT('',(0.00133656424801366,0.00322675153453757,0.0973125000020484));
#19399=CARTESIAN_POINT('',(0.00228165789127562,0.00228165789127562,0.0972187500020484));
#19400=CARTESIAN_POINT('',(0.00322675153453757,0.00133656424801366,0.0971250000020484));
#19401=CARTESIAN_POINT('',(0.00322675153453757,3.95163093841525E-19,0.0970312500020484));
#19402=CARTESIAN_POINT('',(0.00322675153453757,-0.00133656424801366,0.0969375000020483));
#19403=CARTESIAN_POINT('',(0.00228165789127562,-0.00228165789127562,0.0968437500020484));
#19404=CARTESIAN_POINT('',(0.00133656424801366,-0.00322675153453757,0.0967500000020484));
#19405=CARTESIAN_POINT('',(5.92744640762287E-19,-0.00322675153453757,0.0966562500020484));
#19406=CARTESIAN_POINT('',(-0.00133656424801366,-0.00322675153453757,0.0965625000020484));
#19407=CARTESIAN_POINT('',(-0.00228165789127562,-0.00228165789127562,0.0964687500020484));
#19408=CARTESIAN_POINT('',(-0.00322675153453757,-0.00133656424801366,0.0963750000020484));
#19409=CARTESIAN_POINT('',(-0.00322675153453757,0.,0.0962812500020484));
#19410=CARTESIAN_POINT('',(-0.00322675153453757,0.00133656424801366,0.0961875000020484));
#19411=CARTESIAN_POINT('',(-0.00228165789127562,0.00228165789127562,0.0960937500020484));
#19412=CARTESIAN_POINT('',(-0.00133656424801366,0.00322675153453757,0.0960000000020484));
#19413=CARTESIAN_POINT('',(-1.97581546920762E-19,0.00322675153453757,0.0959062500020484));
#19414=CARTESIAN_POINT('',(0.00133656424801366,0.00322675153453757,0.0958125000020483));
#19415=CARTESIAN_POINT('',(0.00228165789127562,0.00228165789127562,0.0957187500020484));
#19416=CARTESIAN_POINT('',(0.00322675153453757,0.00133656424801366,0.0956250000020484));
#19417=CARTESIAN_POINT('',(0.00322675153453757,3.95163093841525E-19,0.0955312500020484));
#19418=CARTESIAN_POINT('',(0.00322675153453757,3.95163093841525E-19,0.0953906250020484));
#19419=CARTESIAN_POINT('',(0.00241485272203757,2.95734165645558E-19,0.107));
#19420=CARTESIAN_POINT('',(0.00241485272203757,2.21800624234168E-19,0.096));
#19421=CARTESIAN_POINT('',(0.00282080212828757,3.45448629743542E-19,0.0957656250010242));
#19422=CARTESIAN_POINT('',(-0.00241485272203757,0.,0.10125));
#19423=CARTESIAN_POINT('',(-0.00241485272203757,0.00100026474860155,0.10115625));
#19424=CARTESIAN_POINT('',(-0.00170755873531956,0.00170755873531956,0.1010625));
#19425=CARTESIAN_POINT('',(-0.00100026474860155,0.00241485272203757,0.10096875));
#19426=CARTESIAN_POINT('',(-1.47867082822779E-19,0.00241485272203757,0.100875));
#19427=CARTESIAN_POINT('',(0.00100026474860155,0.00241485272203757,0.10078125));
#19428=CARTESIAN_POINT('',(0.00170755873531956,0.00170755873531956,0.1006875));
#19429=CARTESIAN_POINT('',(0.00241485272203757,0.00100026474860155,0.10059375));
#19430=CARTESIAN_POINT('',(0.00241485272203757,2.95734165645558E-19,0.1005));
#19431=CARTESIAN_POINT('',(0.00241485272203757,-0.00100026474860155,0.10040625));
#19432=CARTESIAN_POINT('',(0.00170755873531956,-0.00170755873531956,0.1003125));
#19433=CARTESIAN_POINT('',(0.00100026474860155,-0.00241485272203757,0.10021875));
#19434=CARTESIAN_POINT('',(4.43601248468338E-19,-0.00241485272203757,0.100125));
#19435=CARTESIAN_POINT('',(-0.00100026474860155,-0.00241485272203757,0.10003125));
#19436=CARTESIAN_POINT('',(-0.00170755873531956,-0.00170755873531956,0.0999375));
#19437=CARTESIAN_POINT('',(-0.00241485272203757,-0.00100026474860155,0.09984375));
#19438=CARTESIAN_POINT('',(-0.00241485272203757,0.,0.09975));
#19439=CARTESIAN_POINT('',(-0.00241485272203757,0.00100026474860155,0.0996562500000001));
#19440=CARTESIAN_POINT('',(-0.00170755873531956,0.00170755873531956,0.0995625));
#19441=CARTESIAN_POINT('',(-0.00100026474860155,0.00241485272203757,0.09946875));
#19442=CARTESIAN_POINT('',(-1.47867082822779E-19,0.00241485272203757,0.099375));
#19443=CARTESIAN_POINT('',(0.00100026474860155,0.00241485272203757,0.09928125));
#19444=CARTESIAN_POINT('',(0.00170755873531956,0.00170755873531956,0.0991875));
#19445=CARTESIAN_POINT('',(0.00241485272203757,0.00100026474860155,0.0990937499999999));
#19446=CARTESIAN_POINT('',(0.00241485272203757,2.95734165645558E-19,0.099));
#19447=CARTESIAN_POINT('',(0.00241485272203757,-0.00100026474860155,0.09890625));
#19448=CARTESIAN_POINT('',(0.00170755873531956,-0.00170755873531956,0.0988125));
#19449=CARTESIAN_POINT('',(0.00100026474860155,-0.00241485272203757,0.09871875));
#19450=CARTESIAN_POINT('',(4.43601248468338E-19,-0.00241485272203757,0.098625));
#19451=CARTESIAN_POINT('',(-0.00100026474860155,-0.00241485272203757,0.09853125));
#19452=CARTESIAN_POINT('',(-0.00170755873531956,-0.00170755873531956,0.0984375));
#19453=CARTESIAN_POINT('',(-0.00241485272203757,-0.00100026474860155,0.09834375));
#19454=CARTESIAN_POINT('',(-0.00241485272203757,0.,0.09825));
#19455=CARTESIAN_POINT('',(-0.00241485272203757,0.00100026474860155,0.09815625));
#19456=CARTESIAN_POINT('',(-0.00170755873531956,0.00170755873531956,0.0980625));
#19457=CARTESIAN_POINT('',(-0.00100026474860155,0.00241485272203757,0.09796875));
#19458=CARTESIAN_POINT('',(-1.47867082822779E-19,0.00241485272203757,0.097875));
#19459=CARTESIAN_POINT('',(0.00100026474860155,0.00241485272203757,0.09778125));
#19460=CARTESIAN_POINT('',(0.00170755873531956,0.00170755873531956,0.0976875));
#19461=CARTESIAN_POINT('',(0.00241485272203757,0.00100026474860155,0.09759375));
#19462=CARTESIAN_POINT('',(0.00241485272203757,2.95734165645558E-19,0.0975));
#19463=CARTESIAN_POINT('',(0.00241485272203757,-0.00100026474860155,0.0974062500000001));
#19464=CARTESIAN_POINT('',(0.00170755873531956,-0.00170755873531956,0.0973125));
#19465=CARTESIAN_POINT('',(0.00100026474860155,-0.00241485272203757,0.09721875));
#19466=CARTESIAN_POINT('',(4.43601248468338E-19,-0.00241485272203757,0.097125));
#19467=CARTESIAN_POINT('',(-0.00100026474860155,-0.00241485272203757,0.09703125));
#19468=CARTESIAN_POINT('',(-0.00170755873531956,-0.00170755873531956,0.0969375));
#19469=CARTESIAN_POINT('',(-0.00241485272203757,-0.00100026474860155,0.09684375));
#19470=CARTESIAN_POINT('',(-0.00241485272203757,0.,0.09675));
#19471=CARTESIAN_POINT('',(-0.00241485272203757,0.00100026474860155,0.09665625));
#19472=CARTESIAN_POINT('',(-0.00170755873531956,0.00170755873531956,0.0965625));
#19473=CARTESIAN_POINT('',(-0.00100026474860155,0.00241485272203757,0.09646875));
#19474=CARTESIAN_POINT('',(-1.47867082822779E-19,0.00241485272203757,0.096375));
#19475=CARTESIAN_POINT('',(0.00100026474860155,0.00241485272203757,0.0962812500000001));
#19476=CARTESIAN_POINT('',(0.00170755873531956,0.00170755873531956,0.0961875));
#19477=CARTESIAN_POINT('',(0.00241485272203757,0.00100026474860155,0.09609375));
#19478=CARTESIAN_POINT('',(0.00241485272203757,2.95734165645558E-19,0.096));
#19479=CARTESIAN_POINT('',(-0.00322675153453757,0.,0.100781250002048));
#19480=CARTESIAN_POINT('',(-0.00322675153453757,0.00133656424801366,0.100687500002048));
#19481=CARTESIAN_POINT('',(-0.00228165789127562,0.00228165789127562,0.100593750002048));
#19482=CARTESIAN_POINT('',(-0.00133656424801366,0.00322675153453757,0.100500000002048));
#19483=CARTESIAN_POINT('',(-1.97581546920762E-19,0.00322675153453757,0.100406250002048));
#19484=CARTESIAN_POINT('',(0.00133656424801366,0.00322675153453757,0.100312500002048));
#19485=CARTESIAN_POINT('',(0.00228165789127562,0.00228165789127562,0.100218750002048));
#19486=CARTESIAN_POINT('',(0.00322675153453757,0.00133656424801366,0.100125000002048));
#19487=CARTESIAN_POINT('',(0.00322675153453757,3.95163093841525E-19,0.100031250002048));
#19488=CARTESIAN_POINT('',(0.00322675153453757,-0.00133656424801366,0.0999375000020484));
#19489=CARTESIAN_POINT('',(0.00228165789127562,-0.00228165789127562,0.0998437500020484));
#19490=CARTESIAN_POINT('',(0.00133656424801366,-0.00322675153453757,0.0997500000020483));
#19491=CARTESIAN_POINT('',(5.92744640762287E-19,-0.00322675153453757,0.0996562500020484));
#19492=CARTESIAN_POINT('',(-0.00133656424801366,-0.00322675153453757,0.0995625000020484));
#19493=CARTESIAN_POINT('',(-0.00228165789127562,-0.00228165789127562,0.0994687500020484));
#19494=CARTESIAN_POINT('',(-0.00322675153453757,-0.00133656424801366,0.0993750000020484));
#19495=CARTESIAN_POINT('',(-0.00322675153453757,0.,0.0992812500020484));
#19496=CARTESIAN_POINT('',(-0.00322675153453757,0.00133656424801366,0.0991875000020483));
#19497=CARTESIAN_POINT('',(-0.00228165789127562,0.00228165789127562,0.0990937500020484));
#19498=CARTESIAN_POINT('',(-0.00133656424801366,0.00322675153453757,0.0990000000020484));
#19499=CARTESIAN_POINT('',(-1.97581546920762E-19,0.00322675153453757,0.0989062500020484));
#19500=CARTESIAN_POINT('',(0.00133656424801366,0.00322675153453757,0.0988125000020484));
#19501=CARTESIAN_POINT('',(0.00228165789127562,0.00228165789127562,0.0987187500020484));
#19502=CARTESIAN_POINT('',(0.00322675153453757,0.00133656424801366,0.0986250000020484));
#19503=CARTESIAN_POINT('',(0.00322675153453757,3.95163093841525E-19,0.0985312500020484));
#19504=CARTESIAN_POINT('',(0.00322675153453757,-0.00133656424801366,0.0984375000020484));
#19505=CARTESIAN_POINT('',(0.00228165789127562,-0.00228165789127562,0.0983437500020484));
#19506=CARTESIAN_POINT('',(0.00133656424801366,-0.00322675153453757,0.0982500000020484));
#19507=CARTESIAN_POINT('',(5.92744640762287E-19,-0.00322675153453757,0.0981562500020484));
#19508=CARTESIAN_POINT('',(-0.00133656424801366,-0.00322675153453757,0.0980625000020485));
#19509=CARTESIAN_POINT('',(-0.00228165789127562,-0.00228165789127562,0.0979687500020484));
#19510=CARTESIAN_POINT('',(-0.00322675153453757,-0.00133656424801366,0.0978750000020484));
#19511=CARTESIAN_POINT('',(-0.00322675153453757,0.,0.0977812500020484));
#19512=CARTESIAN_POINT('',(-0.00322675153453757,0.00133656424801366,0.0976875000020484));
#19513=CARTESIAN_POINT('',(-0.00228165789127562,0.00228165789127562,0.0975937500020484));
#19514=CARTESIAN_POINT('',(-0.00133656424801366,0.00322675153453757,0.0975000000020484));
#19515=CARTESIAN_POINT('',(-1.97581546920762E-19,0.00322675153453757,0.0974062500020484));
#19516=CARTESIAN_POINT('',(0.00133656424801366,0.00322675153453757,0.0973125000020484));
#19517=CARTESIAN_POINT('',(0.00228165789127562,0.00228165789127562,0.0972187500020484));
#19518=CARTESIAN_POINT('',(0.00322675153453757,0.00133656424801366,0.0971250000020484));
#19519=CARTESIAN_POINT('',(0.00322675153453757,3.95163093841525E-19,0.0970312500020484));
#19520=CARTESIAN_POINT('',(0.00322675153453757,-0.00133656424801366,0.0969375000020484));
#19521=CARTESIAN_POINT('',(0.00228165789127562,-0.00228165789127562,0.0968437500020484));
#19522=CARTESIAN_POINT('',(0.00133656424801366,-0.00322675153453757,0.0967500000020484));
#19523=CARTESIAN_POINT('',(5.92744640762287E-19,-0.00322675153453757,0.0966562500020484));
#19524=CARTESIAN_POINT('',(-0.00133656424801366,-0.00322675153453757,0.0965625000020484));
#19525=CARTESIAN_POINT('',(-0.00228165789127562,-0.00228165789127562,0.0964687500020484));
#19526=CARTESIAN_POINT('',(-0.00322675153453757,-0.00133656424801366,0.0963750000020484));
#19527=CARTESIAN_POINT('',(-0.00322675153453757,0.,0.0962812500020484));
#19528=CARTESIAN_POINT('',(-0.00322675153453757,0.00133656424801366,0.0961875000020484));
#19529=CARTESIAN_POINT('',(-0.00228165789127562,0.00228165789127562,0.0960937500020484));
#19530=CARTESIAN_POINT('',(-0.00133656424801366,0.00322675153453757,0.0960000000020484));
#19531=CARTESIAN_POINT('',(-1.97581546920762E-19,0.00322675153453757,0.0959062500020484));
#19532=CARTESIAN_POINT('',(0.00133656424801366,0.00322675153453757,0.0958125000020483));
#19533=CARTESIAN_POINT('',(0.00228165789127562,0.00228165789127562,0.0957187500020484));
#19534=CARTESIAN_POINT('',(0.00322675153453757,0.00133656424801366,0.0956250000020484));
#19535=CARTESIAN_POINT('',(0.00322675153453757,3.95163093841525E-19,0.0955312500020484));
#19536=CARTESIAN_POINT('',(-0.00120116781157934,0.00209492471405489,0.101));
#19537=CARTESIAN_POINT('',(-0.00208526276506858,0.00177414214407331,0.101));
#19538=CARTESIAN_POINT('',(-0.00271974082590136,0.000930774313530578,0.101));
#19539=CARTESIAN_POINT('',(-0.00284786542392977,0.,0.101));
#19540=CARTESIAN_POINT('',(-0.00120116781157934,0.00209492471405489,0.101));
#19541=CARTESIAN_POINT('',(-0.00284786542392979,0.,0.101));
#19542=CARTESIAN_POINT('',(-0.00282080212828757,0.,0.101015625001024));
#19543=CARTESIAN_POINT('',(-0.00241485272203757,0.,0.09675));
#19544=CARTESIAN_POINT('',(-0.00241485272203757,0.00100026474860155,0.09665625));
#19545=CARTESIAN_POINT('',(-0.00170755873531956,0.00170755873531956,0.0965625));
#19546=CARTESIAN_POINT('',(-0.00100026474860155,0.00241485272203757,0.09646875));
#19547=CARTESIAN_POINT('',(-1.47867082822779E-19,0.00241485272203757,0.096375));
#19548=CARTESIAN_POINT('',(0.00100026474860155,0.00241485272203757,0.0962812500000001));
#19549=CARTESIAN_POINT('',(0.00170755873531956,0.00170755873531956,0.0961875));
#19550=CARTESIAN_POINT('',(0.00241485272203757,0.00100026474860155,0.09609375));
#19551=CARTESIAN_POINT('',(0.00241485272203757,2.95734165645558E-19,0.096));
#19552=CARTESIAN_POINT('',(-0.00241485272203757,0.,0.09675));
#19553=CARTESIAN_POINT('',(0.00241485272203757,2.95734165645558E-19,0.0975));
#19554=CARTESIAN_POINT('',(0.00241485272203757,-0.00100026474860155,0.0974062500000001));
#19555=CARTESIAN_POINT('',(0.00170755873531956,-0.00170755873531956,0.0973125));
#19556=CARTESIAN_POINT('',(0.00100026474860155,-0.00241485272203757,0.09721875));
#19557=CARTESIAN_POINT('',(4.43601248468338E-19,-0.00241485272203757,0.097125));
#19558=CARTESIAN_POINT('',(-0.00100026474860155,-0.00241485272203757,0.09703125));
#19559=CARTESIAN_POINT('',(-0.00170755873531956,-0.00170755873531956,0.0969375));
#19560=CARTESIAN_POINT('',(-0.00241485272203757,-0.00100026474860155,0.09684375));
#19561=CARTESIAN_POINT('',(-0.00241485272203757,0.,0.09675));
#19562=CARTESIAN_POINT('',(0.00241485272203757,2.95734165645558E-19,0.0975));
#19563=CARTESIAN_POINT('',(-0.00241485272203757,0.,0.09825));
#19564=CARTESIAN_POINT('',(-0.00241485272203757,0.00100026474860155,0.09815625));
#19565=CARTESIAN_POINT('',(-0.00170755873531956,0.00170755873531956,0.0980625));
#19566=CARTESIAN_POINT('',(-0.00100026474860155,0.00241485272203757,0.09796875));
#19567=CARTESIAN_POINT('',(-1.47867082822779E-19,0.00241485272203757,0.097875));
#19568=CARTESIAN_POINT('',(0.00100026474860155,0.00241485272203757,0.09778125));
#19569=CARTESIAN_POINT('',(0.00170755873531956,0.00170755873531956,0.0976875));
#19570=CARTESIAN_POINT('',(0.00241485272203757,0.00100026474860155,0.09759375));
#19571=CARTESIAN_POINT('',(0.00241485272203757,2.95734165645558E-19,0.0975));
#19572=CARTESIAN_POINT('',(-0.00241485272203757,0.,0.09825));
#19573=CARTESIAN_POINT('',(0.00241485272203757,2.95734165645558E-19,0.099));
#19574=CARTESIAN_POINT('',(0.00241485272203757,-0.00100026474860155,0.09890625));
#19575=CARTESIAN_POINT('',(0.00170755873531956,-0.00170755873531956,0.0988125));
#19576=CARTESIAN_POINT('',(0.00100026474860155,-0.00241485272203757,0.09871875));
#19577=CARTESIAN_POINT('',(4.43601248468338E-19,-0.00241485272203757,0.098625));
#19578=CARTESIAN_POINT('',(-0.00100026474860155,-0.00241485272203757,0.0985312500000001));
#19579=CARTESIAN_POINT('',(-0.00170755873531956,-0.00170755873531956,0.0984375));
#19580=CARTESIAN_POINT('',(-0.00241485272203757,-0.00100026474860155,0.09834375));
#19581=CARTESIAN_POINT('',(-0.00241485272203757,0.,0.09825));
#19582=CARTESIAN_POINT('',(0.00241485272203757,2.95734165645558E-19,0.099));
#19583=CARTESIAN_POINT('',(-0.00241485272203757,0.,0.09975));
#19584=CARTESIAN_POINT('',(-0.00241485272203757,0.00100026474860155,0.0996562500000001));
#19585=CARTESIAN_POINT('',(-0.00170755873531956,0.00170755873531956,0.0995625));
#19586=CARTESIAN_POINT('',(-0.00100026474860155,0.00241485272203757,0.09946875));
#19587=CARTESIAN_POINT('',(-1.47867082822779E-19,0.00241485272203757,0.099375));
#19588=CARTESIAN_POINT('',(0.00100026474860155,0.00241485272203757,0.09928125));
#19589=CARTESIAN_POINT('',(0.00170755873531956,0.00170755873531956,0.0991875));
#19590=CARTESIAN_POINT('',(0.00241485272203757,0.00100026474860155,0.0990937499999999));
#19591=CARTESIAN_POINT('',(0.00241485272203757,2.95734165645558E-19,0.099));
#19592=CARTESIAN_POINT('',(-0.00241485272203757,0.,0.09975));
#19593=CARTESIAN_POINT('',(0.00241485272203757,2.95734165645558E-19,0.1005));
#19594=CARTESIAN_POINT('',(0.00241485272203757,-0.00100026474860155,0.10040625));
#19595=CARTESIAN_POINT('',(0.00170755873531956,-0.00170755873531956,0.1003125));
#19596=CARTESIAN_POINT('',(0.00100026474860155,-0.00241485272203757,0.10021875));
#19597=CARTESIAN_POINT('',(4.43601248468338E-19,-0.00241485272203757,0.100125));
#19598=CARTESIAN_POINT('',(-0.00100026474860155,-0.00241485272203757,0.10003125));
#19599=CARTESIAN_POINT('',(-0.00170755873531956,-0.00170755873531956,0.0999375));
#19600=CARTESIAN_POINT('',(-0.00241485272203757,-0.00100026474860155,0.09984375));
#19601=CARTESIAN_POINT('',(-0.00241485272203757,0.,0.09975));
#19602=CARTESIAN_POINT('',(0.00241485272203757,2.95734165645558E-19,0.1005));
#19603=CARTESIAN_POINT('',(-0.00120116781157934,0.00209492471405489,0.101));
#19604=CARTESIAN_POINT('',(-0.000643189913586848,0.00241485272203757,0.100935283094534));
#19605=CARTESIAN_POINT('',(-1.47867082822779E-19,0.00241485272203757,0.100875));
#19606=CARTESIAN_POINT('',(0.00100026474860155,0.00241485272203757,0.10078125));
#19607=CARTESIAN_POINT('',(0.00170755873531956,0.00170755873531956,0.1006875));
#19608=CARTESIAN_POINT('',(0.00241485272203757,0.00100026474860155,0.10059375));
#19609=CARTESIAN_POINT('',(0.00241485272203757,2.95734165645558E-19,0.1005));
#19610=CARTESIAN_POINT('',(0.00322675153453757,3.95163093841525E-19,0.0953906250020484));
#19611=CARTESIAN_POINT('',(-0.00241485272203757,0.,0.100687500002048));
#19612=CARTESIAN_POINT('',(-0.00241485272203757,9.85780552151861E-20,0.101));
#19613=CARTESIAN_POINT('',(0.,0.,0.101));
#19614=CARTESIAN_POINT('',(0.,0.00455,0.101));
#19615=CARTESIAN_POINT('',(0.,0.,0.101));
#19616=CARTESIAN_POINT('',(-0.00455,0.,0.101));
#19617=CARTESIAN_POINT('',(0.,0.,0.101));
#19618=CARTESIAN_POINT('',(-1.00349973962234E-18,-0.00241485272203757,0.09473856967));
#19619=CARTESIAN_POINT('',(0.00482970544407513,-0.00241485272203757,0.09473856967));
#19620=CARTESIAN_POINT('',(0.00482970544407514,0.00241485272203756,0.09473856967));
#19621=CARTESIAN_POINT('',(2.95093640562077E-18,0.00241485272203757,0.09473856967));
#19622=CARTESIAN_POINT('',(-2.19497575959325E-18,-0.00241485272203757,0.0945272023210931));
#19623=CARTESIAN_POINT('',(0.00482970544407514,-0.00241485272203757,0.094527202321093));
#19624=CARTESIAN_POINT('',(0.00482970544407514,0.00241485272203757,0.094527202321093));
#19625=CARTESIAN_POINT('',(1.2443477489079E-18,0.00241485272203757,0.0945272023210931));
#19626=CARTESIAN_POINT('',(-3.39567156950461E-18,-0.00248323514802505,0.0943272023210931));
#19627=CARTESIAN_POINT('',(0.00496647029605009,-0.00248323514802505,0.0943272023210931));
#19628=CARTESIAN_POINT('',(0.0049664702960501,0.00248323514802504,0.0943272023210931));
#19629=CARTESIAN_POINT('',(-3.49524386054981E-19,0.00248323514802505,0.0943272023210931));
#19630=CARTESIAN_POINT('',(-4.60558716935644E-18,-0.00262,0.09413856967));
#19631=CARTESIAN_POINT('',(0.00524,-0.00262000000000001,0.09413856967));
#19632=CARTESIAN_POINT('',(0.00524000000000001,0.00262,0.09413856967));
#19633=CARTESIAN_POINT('',(-1.83067999926848E-18,0.00262,0.09413856967));
#19634=CARTESIAN_POINT('',(-3.08295813511083E-19,-0.00241485272203757,0.09473856967));
#19635=CARTESIAN_POINT('',(-2.95734165645558E-19,-0.00241485272203757,0.0944215186466397));
#19636=CARTESIAN_POINT('',(-3.20857461376607E-19,-0.00262,0.09413856967));
#19637=CARTESIAN_POINT('',(-3.08295813511083E-19,-0.00241485272203757,0.09473856967));
#19638=CARTESIAN_POINT('',(-3.20857461376607E-19,-0.00262,0.09413856967));
#19639=CARTESIAN_POINT('',(0.,0.,0.09473856967));
#19640=CARTESIAN_POINT('',(0.,0.00241485272203757,0.09473856967));
#19641=CARTESIAN_POINT('',(0.,0.00241485272203757,0.09473856967));
#19642=CARTESIAN_POINT('',(0.,0.00241485272203757,0.0944215186466397));
#19643=CARTESIAN_POINT('',(0.,0.00262,0.09413856967));
#19644=CARTESIAN_POINT('',(0.,0.00262,0.09413856967));
#19645=CARTESIAN_POINT('',(0.,0.,0.09413856967));
#19646=CARTESIAN_POINT('',(0.,0.00262,0.09413856967));
#19647=CARTESIAN_POINT('',(0.,0.,0.09413856967));
#19648=CARTESIAN_POINT('',(0.,0.,0.09413856967));
#19649=CARTESIAN_POINT('',(0.00455,0.,0.09413856967));
#19650=CARTESIAN_POINT('',(0.,0.,0.1029));
#19651=CARTESIAN_POINT('',(0.,0.,0.1029));
#19652=CARTESIAN_POINT('',(0.00455,0.,0.1029));
#19653=CARTESIAN_POINT('',(0.,0.,0.1029));
#19654=CARTESIAN_POINT('',(0.00505,0.,0.1029));
#19655=CARTESIAN_POINT('',(-0.0337929399400243,0.0154689110867544,0.073));
#19656=CARTESIAN_POINT('',(-0.0320429399400243,0.0185,0.083));
#19657=CARTESIAN_POINT('',(-0.0337929399400243,0.0154689110867544,0.083));
#19658=CARTESIAN_POINT('',(-0.0302929399400243,0.0215310889132454,0.083));
#19659=CARTESIAN_POINT('',(-0.0302929399400243,0.0215310889132454,0.073));
#19660=CARTESIAN_POINT('',(-0.0302929399400243,0.0215310889132454,0.081));
#19661=CARTESIAN_POINT('',(-0.0320429399400243,0.0185,0.081));
#19662=CARTESIAN_POINT('',(-0.0337929399400243,0.0154689110867544,0.081));
#19663=CARTESIAN_POINT('',(-0.0337929399400243,0.0154689110867544,0.073));
#19664=CARTESIAN_POINT('',(-0.0355249907475932,0.0164689110867544,0.073));
#19665=CARTESIAN_POINT('',(-0.0337749907475932,0.0195,0.083));
#19666=CARTESIAN_POINT('',(-0.0320249907475932,0.0225310889132454,0.083));
#19667=CARTESIAN_POINT('',(-0.0355249907475932,0.0164689110867544,0.083));
#19668=CARTESIAN_POINT('',(-0.0355249907475932,0.0164689110867544,0.073));
#19669=CARTESIAN_POINT('',(-0.0355249907475932,0.0164689110867544,0.081));
#19670=CARTESIAN_POINT('',(-0.0337749907475932,0.0195,0.081));
#19671=CARTESIAN_POINT('',(-0.0320249907475932,0.0225310889132454,0.081));
#19672=CARTESIAN_POINT('',(-0.0320249907475932,0.0225310889132454,0.073));
#19673=CARTESIAN_POINT('',(-0.0346589653438087,0.0159689110867544,0.073));
#19674=CARTESIAN_POINT('',(-0.0346589653438087,0.0159689110867544,0.083));
#19675=CARTESIAN_POINT('',(-0.0346589653438087,0.0159689110867544,0.081));
#19676=CARTESIAN_POINT('',(0.00350000000000026,-0.037,0.073));
#19677=CARTESIAN_POINT('',(2.393918396848E-16,-0.037,0.083));
#19678=CARTESIAN_POINT('',(0.00350000000000026,-0.037,0.083));
#19679=CARTESIAN_POINT('',(-0.00349999999999974,-0.037,0.083));
#19680=CARTESIAN_POINT('',(-0.00349999999999974,-0.037,0.073));
#19681=CARTESIAN_POINT('',(-0.00349999999999974,-0.037,0.081));
#19682=CARTESIAN_POINT('',(2.393918396848E-16,-0.037,0.081));
#19683=CARTESIAN_POINT('',(0.00350000000000026,-0.037,0.081));
#19684=CARTESIAN_POINT('',(0.00350000000000026,-0.037,0.073));
#19685=CARTESIAN_POINT('',(0.00350000000000027,-0.039,0.073));
#19686=CARTESIAN_POINT('',(2.74086309204335E-16,-0.039,0.083));
#19687=CARTESIAN_POINT('',(-0.00349999999999973,-0.039,0.083));
#19688=CARTESIAN_POINT('',(0.00350000000000028,-0.039,0.083));
#19689=CARTESIAN_POINT('',(0.00350000000000027,-0.039,0.073));
#19690=CARTESIAN_POINT('',(0.00350000000000028,-0.039,0.081));
#19691=CARTESIAN_POINT('',(2.74086309204335E-16,-0.039,0.081));
#19692=CARTESIAN_POINT('',(-0.00349999999999973,-0.039,0.081));
#19693=CARTESIAN_POINT('',(-0.00349999999999972,-0.039,0.073));
#19694=CARTESIAN_POINT('',(0.00350000000000027,-0.038,0.073));
#19695=CARTESIAN_POINT('',(0.00350000000000027,-0.038,0.083));
#19696=CARTESIAN_POINT('',(0.00350000000000027,-0.038,0.081));
#19697=CARTESIAN_POINT('',(0.0302929399400243,0.0215310889132454,0.073));
#19698=CARTESIAN_POINT('',(0.0320429399400243,0.0185,0.083));
#19699=CARTESIAN_POINT('',(0.0302929399400243,0.0215310889132454,0.083));
#19700=CARTESIAN_POINT('',(0.0337929399400242,0.0154689110867544,0.083));
#19701=CARTESIAN_POINT('',(0.0337929399400242,0.0154689110867544,0.073));
#19702=CARTESIAN_POINT('',(0.0337929399400242,0.0154689110867544,0.081));
#19703=CARTESIAN_POINT('',(0.0320429399400243,0.0185,0.081));
#19704=CARTESIAN_POINT('',(0.0302929399400243,0.0215310889132454,0.081));
#19705=CARTESIAN_POINT('',(0.0302929399400243,0.0215310889132454,0.073));
#19706=CARTESIAN_POINT('',(0.0320249907475932,0.0225310889132454,0.073));
#19707=CARTESIAN_POINT('',(0.0337749907475932,0.0195,0.083));
#19708=CARTESIAN_POINT('',(0.0355249907475932,0.0164689110867544,0.083));
#19709=CARTESIAN_POINT('',(0.0320249907475932,0.0225310889132454,0.083));
#19710=CARTESIAN_POINT('',(0.0320249907475932,0.0225310889132454,0.073));
#19711=CARTESIAN_POINT('',(0.0320249907475932,0.0225310889132454,0.081));
#19712=CARTESIAN_POINT('',(0.0337749907475932,0.0195,0.081));
#19713=CARTESIAN_POINT('',(0.0355249907475932,0.0164689110867544,0.081));
#19714=CARTESIAN_POINT('',(0.0355249907475932,0.0164689110867544,0.073));
#19715=CARTESIAN_POINT('',(0.0311589653438087,0.0220310889132454,0.073));
#19716=CARTESIAN_POINT('',(0.0311589653438087,0.0220310889132454,0.083));
#19717=CARTESIAN_POINT('',(0.0311589653438087,0.0220310889132454,0.081));
#19718=CARTESIAN_POINT('',(4.47686656242088E-16,-0.044397,0.0815014));
#19719=CARTESIAN_POINT('',(-1.32786462810487E-16,0.043,0.0815014));
#19720=CARTESIAN_POINT('',(-1.43180183778462E-16,0.04597688,0.0815014));
#19721=CARTESIAN_POINT('',(-1.32786462810487E-16,0.043,0.0815014));
#19722=CARTESIAN_POINT('',(-1.3766406224085E-16,0.044397,0.0815014));
#19723=CARTESIAN_POINT('',(4.47686656242088E-16,-0.044397,0.0815014));
#19724=CARTESIAN_POINT('',(-0.043,1.7347234759768E-17,0.0815014));
#19725=CARTESIAN_POINT('',(-0.04597688,1.7347234759768E-17,0.0815014));
#19726=CARTESIAN_POINT('',(-0.043,1.7347234759768E-17,0.0815014));
#19727=CARTESIAN_POINT('',(-0.044397,1.7347234759768E-17,0.0815014));
#19728=CARTESIAN_POINT('',(4.47686656242088E-16,-0.044397,0.0815014));
#19729=CARTESIAN_POINT('',(4.33053857950996E-16,-0.043,0.0815014));
#19730=CARTESIAN_POINT('',(4.64235020854922E-16,-0.04597688,0.0815014));
#19731=CARTESIAN_POINT('',(4.33053857950996E-16,-0.043,0.0815014));
#19732=CARTESIAN_POINT('',(4.47686656242088E-16,-0.044397,0.0815014));
#19733=CARTESIAN_POINT('',(4.47686656242088E-16,-0.044397,0.0815014));
#19734=CARTESIAN_POINT('',(0.043,-1.7347234759768E-17,0.0815014));
#19735=CARTESIAN_POINT('',(0.04597688,-1.7347234759768E-17,0.0815014));
#19736=CARTESIAN_POINT('',(0.043,-1.7347234759768E-17,0.0815014));
#19737=CARTESIAN_POINT('',(0.044397,-1.7347234759768E-17,0.0815014));
#19738=CARTESIAN_POINT('',(0.,0.,0.081));
#19739=CARTESIAN_POINT('',(-0.02598076211353,-0.0150000000000018,0.081));
#19740=CARTESIAN_POINT('',(-0.0219807621135261,-0.0150000000000018,0.081));
#19741=CARTESIAN_POINT('',(0.0259807621135363,-0.0149999999999982,0.081));
#19742=CARTESIAN_POINT('',(0.029980762113539,-0.0149999999999982,0.081));
#19743=CARTESIAN_POINT('',(0.,0.03,0.081));
#19744=CARTESIAN_POINT('',(0.004,0.03,0.081));
#19745=CARTESIAN_POINT('',(0.,0.,0.081));
#19746=CARTESIAN_POINT('',(0.00755,0.,0.081));
#19747=CARTESIAN_POINT('',(0.,0.,0.081));
#19748=CARTESIAN_POINT('',(0.05,0.,0.081));
#19749=CARTESIAN_POINT('',(0.043,-1.7347234759768E-17,0.081));
#19750=CARTESIAN_POINT('',(0.044397,-1.7347234759768E-17,0.081));
#19751=CARTESIAN_POINT('',(4.33053857950996E-16,-0.043,0.081));
#19752=CARTESIAN_POINT('',(4.47686656242088E-16,-0.044397,0.081));
#19753=CARTESIAN_POINT('',(-0.043,1.7347234759768E-17,0.081));
#19754=CARTESIAN_POINT('',(-0.044397,1.7347234759768E-17,0.081));
#19755=CARTESIAN_POINT('',(-1.32786462810487E-16,0.043,0.081));
#19756=CARTESIAN_POINT('',(-1.3766406224085E-16,0.044397,0.081));
#19757=CARTESIAN_POINT('',(0.0346589653438087,0.0159689110867544,0.081));
#19758=CARTESIAN_POINT('',(-0.00349999999999973,-0.038,0.081));
#19759=CARTESIAN_POINT('',(-0.0311589653438087,0.0220310889132454,0.081));
#19760=CARTESIAN_POINT('',(-0.0175,0.0303108891324553,0.081));
#19761=CARTESIAN_POINT('',(-0.0075,0.0303108891324553,0.081));
#19762=CARTESIAN_POINT('',(0.,0.,0.083));
#19763=CARTESIAN_POINT('',(-0.02598076211353,-0.0150000000000018,0.083));
#19764=CARTESIAN_POINT('',(-0.0219807621135261,-0.0150000000000018,0.083));
#19765=CARTESIAN_POINT('',(0.,0.03,0.083));
#19766=CARTESIAN_POINT('',(0.004,0.03,0.083));
#19767=CARTESIAN_POINT('',(0.,0.,0.083));
#19768=CARTESIAN_POINT('',(0.05,0.,0.083));
#19769=CARTESIAN_POINT('',(0.,0.,0.083));
#19770=CARTESIAN_POINT('',(0.00755,0.,0.083));
#19771=CARTESIAN_POINT('',(0.0259807621135363,-0.0149999999999982,0.083));
#19772=CARTESIAN_POINT('',(0.029980762113539,-0.0149999999999982,0.083));
#19773=CARTESIAN_POINT('',(0.043,-1.7347234759768E-17,0.083));
#19774=CARTESIAN_POINT('',(0.04597688,-1.7347234759768E-17,0.083));
#19775=CARTESIAN_POINT('',(4.33053857950996E-16,-0.043,0.083));
#19776=CARTESIAN_POINT('',(4.64235020854922E-16,-0.04597688,0.083));
#19777=CARTESIAN_POINT('',(-0.043,1.7347234759768E-17,0.083));
#19778=CARTESIAN_POINT('',(-0.04597688,1.7347234759768E-17,0.083));
#19779=CARTESIAN_POINT('',(-1.32786462810487E-16,0.043,0.083));
#19780=CARTESIAN_POINT('',(-1.43180183778462E-16,0.04597688,0.083));
#19781=CARTESIAN_POINT('',(0.0346589653438087,0.0159689110867544,0.083));
#19782=CARTESIAN_POINT('',(-0.00349999999999973,-0.038,0.083));
#19783=CARTESIAN_POINT('',(-0.0311589653438087,0.0220310889132454,0.083));
#19784=CARTESIAN_POINT('',(-0.0175,0.0303108891324553,0.083));
#19785=CARTESIAN_POINT('',(-0.0075,0.0303108891324553,0.083));
#19786=CARTESIAN_POINT('',(0.,0.,0.107));
#19787=CARTESIAN_POINT('',(0.,0.,0.107));
#19788=CARTESIAN_POINT('',(0.00755,0.,0.107));
#19789=CARTESIAN_POINT('',(0.,0.,0.107));
#19790=CARTESIAN_POINT('',(0.00505,0.,0.107));
#19791=CARTESIAN_POINT('',(0.,0.,0.073));
#19792=CARTESIAN_POINT('',(0.,0.,0.073));
#19793=CARTESIAN_POINT('',(0.00755,0.,0.073));
#19794=CARTESIAN_POINT('',(0.,0.,0.073));
#19795=CARTESIAN_POINT('',(0.00555,0.,0.073));
#19796=CARTESIAN_POINT('',(0.,0.,0.073));
#19797=CARTESIAN_POINT('',(0.,0.,0.074));
#19798=CARTESIAN_POINT('',(0.00455,0.,0.074));
#19799=CARTESIAN_POINT('',(0.,0.,0.073));
#19800=CARTESIAN_POINT('',(0.,0.,0.073));
#19801=CARTESIAN_POINT('',(0.,0.,0.073));
#19802=CARTESIAN_POINT('',(0.,0.,0.083));
#19803=CARTESIAN_POINT('',(0.,0.03,0.083));
#19804=CARTESIAN_POINT('',(0.0259807621135363,-0.0149999999999982,0.083));
#19805=CARTESIAN_POINT('',(-0.02598076211353,-0.0150000000000018,0.083));
#19806=CARTESIAN_POINT('',(0.043,-1.7347234759768E-17,0.083));
#19807=CARTESIAN_POINT('',(0.043,-1.7347234759768E-17,0.083));
#19808=CARTESIAN_POINT('',(4.33053857950996E-16,-0.043,0.083));
#19809=CARTESIAN_POINT('',(4.33053857950996E-16,-0.043,0.083));
#19810=CARTESIAN_POINT('',(-0.043,1.7347234759768E-17,0.083));
#19811=CARTESIAN_POINT('',(-0.043,1.7347234759768E-17,0.083));
#19812=CARTESIAN_POINT('',(-1.32786462810487E-16,0.043,0.083));
#19813=CARTESIAN_POINT('',(-1.32786462810487E-16,0.043,0.083));
#19814=CARTESIAN_POINT('',(0.0346589653438087,0.0159689110867544,0.073));
#19815=CARTESIAN_POINT('',(-0.00349999999999973,-0.038,0.073));
#19816=CARTESIAN_POINT('',(-0.0311589653438087,0.0220310889132454,0.073));
#19817=CARTESIAN_POINT('',(-0.0175,0.0303108891324553,0.107));
#19818=CARTESIAN_POINT('',(0.,0.,0.1029));
#19819=CARTESIAN_POINT('',(0.,0.,0.107));
#19820=CARTESIAN_POINT('',(0.,0.,0.09473856967));
#19821=CARTESIAN_POINT('',(0.,0.,0.074));
#19822=CARTESIAN_POINT('',(1.42442054663212E-18,0.00241485272203757,0.09473856967));
#19823=CARTESIAN_POINT('',(-0.00482970544407513,0.00241485272203757,0.09473856967));
#19824=CARTESIAN_POINT('',(-0.00482970544407514,-0.00241485272203756,0.09473856967));
#19825=CARTESIAN_POINT('',(-3.37185721263055E-18,-0.00241485272203757,0.09473856967));
#19826=CARTESIAN_POINT('',(2.61589656660303E-18,0.00241485272203757,0.0945272023210931));
#19827=CARTESIAN_POINT('',(-0.00482970544407514,0.00241485272203757,0.094527202321093));
#19828=CARTESIAN_POINT('',(-0.00482970544407514,-0.00241485272203757,0.094527202321093));
#19829=CARTESIAN_POINT('',(-1.66526855591768E-18,-0.00241485272203757,0.0945272023210931));
#19830=CARTESIAN_POINT('',(3.8165923765144E-18,0.00248323514802505,0.0943272023210931));
#19831=CARTESIAN_POINT('',(-0.00496647029605009,0.00248323514802505,0.0943272023210931));
#19832=CARTESIAN_POINT('',(-0.0049664702960501,-0.00248323514802504,0.0943272023210931));
#19833=CARTESIAN_POINT('',(-7.13964209548004E-20,-0.00248323514802505,0.0943272023210931));
#19834=CARTESIAN_POINT('',(5.02650797636622E-18,0.00262,0.09413856967));
#19835=CARTESIAN_POINT('',(-0.00524,0.00262000000000001,0.09413856967));
#19836=CARTESIAN_POINT('',(-0.00524000000000001,-0.00262,0.09413856967));
#19837=CARTESIAN_POINT('',(1.4097591922587E-18,-0.00262,0.09413856967));
#45463=MECHANICAL_DESIGN_GEOMETRIC_PRESENTATION_REPRESENTATION('',(#13529),#45464);
#45464=(
GEOMETRIC_REPRESENTATION_CONTEXT(3)
GLOBAL_UNCERTAINTY_ASSIGNED_CONTEXT((#45492))
GLOBAL_UNIT_ASSIGNED_CONTEXT((#45522,#45521,#45520))
REPRESENTATION_CONTEXT('MAS-690','TOP_LEVEL_ASSEMBLY_PART')
);
#45465=(
GEOMETRIC_REPRESENTATION_CONTEXT(3)
GLOBAL_UNCERTAINTY_ASSIGNED_CONTEXT((#45493))
GLOBAL_UNIT_ASSIGNED_CONTEXT((#45522,#45521,#45520))
REPRESENTATION_CONTEXT('Top_acces_nozzle_supporter','COMPONENT_PART')
);
#45492=UNCERTAINTY_MEASURE_WITH_UNIT(LENGTH_MEASURE(1.E-8),#45522,
'DISTANCE_ACCURACY_VALUE','Maximum Tolerance applied to model');
#45493=UNCERTAINTY_MEASURE_WITH_UNIT(LENGTH_MEASURE(2.E-5),#45522,
'DISTANCE_ACCURACY_VALUE','Maximum Tolerance applied to model');
#45520=(
NAMED_UNIT(*)
SI_UNIT($,.STERADIAN.)
SOLID_ANGLE_UNIT()
);
#45521=(
NAMED_UNIT(*)
PLANE_ANGLE_UNIT()
SI_UNIT($,.RADIAN.)
);
#45522=(
LENGTH_UNIT()
NAMED_UNIT(*)
SI_UNIT($,.METRE.)
);
#45524=PRODUCT_DEFINITION_SHAPE('','',#45586);
#45586=PRODUCT_DEFINITION('','',#45642,#45614);
#45614=PRODUCT_DEFINITION_CONTEXT('',#45782,'design');
#45642=PRODUCT_DEFINITION_FORMATION_WITH_SPECIFIED_SOURCE('','',#45698,
 .NOT_KNOWN.);
#45698=PRODUCT('Top_acces_nozzle_supporter',
'Top_acces_nozzle_supporter','Top_acces_nozzle_supporter',(#45754));
#45754=PRODUCT_CONTEXT('',#45782,'mechanical');
#45782=APPLICATION_CONTEXT('managed model based 3d engineering');
ENDSEC;
END-ISO-10303-21;
